ISO-10303-21;
HEADER;
FILE_DESCRIPTION (('STEP AP214'),
    '1' );
FILE_NAME ('Bolt-Mounted Retaining Cylinder.step',
    '2026-10-19T17:36:30',
    ( '' ),
    ( '' ),
    'SwSTEP 2.0',
    'SolidWorks 2025',
    '' );
FILE_SCHEMA (( 'AUTOMOTIVE_DESIGN' ));
ENDSEC;

DATA;
#7=CIRCLE ( 'NONE', #4871, 25.00000000000000000 ) ;
#29=CIRCLE ( 'NONE', #3272, 28.00000000000000000 ) ;
#32=CARTESIAN_POINT ( 'NONE',  ( -2.507735966467860678, 54.33796433351858468, -24.87540749666489148 ) ) ;
#36=B_SPLINE_CURVE_WITH_KNOTS ( 'NONE', 3,
 ( #5460, #12302, #630, #1640, #3542, #1581, #10446, #9451, #12364, #9328, #4495, #7414, #1699, #2590, #753, #3601, #7540, #9388 ),
 .UNSPECIFIED., .F., .F.,
 ( 4, 2, 2, 2, 2, 2, 2, 2, 4 ),
 ( 0.000000000000000000, 0.0009797303413002214287, 0.001959460682600442857, 0.002939191023900664286, 0.003918921365200885715, 0.004898651706501107143, 0.005878382047801328572, 0.006858112389101550001, 0.007837842730401771429 ),
 .UNSPECIFIED. ) ;
#38=CARTESIAN_POINT ( 'NONE',  ( 9.468091998436410250, 23.23472460790263838, -26.35081933702187129 ) ) ;
#50=DIRECTION ( 'NONE',  ( -0.000000000000000000, -0.000000000000000000, 1.000000000000000000 ) ) ;
#67=EDGE_CURVE ( 'NONE', #6224, #4669, #12253, .T. ) ;
#76=( NAMED_UNIT ( * ) SI_UNIT ( $, .STERADIAN. ) SOLID_ANGLE_UNIT ( ) );
#90=CIRCLE ( 'NONE', #7986, 25.00000000000000000 ) ;
#97=CARTESIAN_POINT ( 'NONE',  ( -4.999999999999999112, 50.32713193883511593, -24.49489742783179125 ) ) ;
#99=CARTESIAN_POINT ( 'NONE',  ( 0.000000000000000000, 0.000000000000000000, -28.00000000000000355 ) ) ;
#122=CARTESIAN_POINT ( 'NONE',  ( 4.337695533240938595, 47.49144378315899928, 27.66258726422904246 ) ) ;
#126=ORIENTED_EDGE ( 'NONE', *, *, #9586, .F. ) ;
#130=DIRECTION ( 'NONE',  ( 1.000000000000000000, 0.000000000000000000, 0.000000000000000000 ) ) ;
#134=CARTESIAN_POINT ( 'NONE',  ( -10.00000000000000355, 20.00000000000000355, -22.91287847477919826 ) ) ;
#138=EDGE_LOOP ( 'NONE', ( #6362, #6499, #12399, #3015, #10689, #7029 ) ) ;
#144=CARTESIAN_POINT ( 'NONE',  ( 6.107750375176497215, 12.05530454078378000, -27.33128490115649711 ) ) ;
#160=EDGE_CURVE ( 'NONE', #6466, #7533, #9507, .T. ) ;
#166=CARTESIAN_POINT ( 'NONE',  ( -1.612284376581284429, 54.74427448601975499, 27.95519242099699397 ) ) ;
#194=CYLINDRICAL_SURFACE ( 'NONE', #2295, 10.00000000000000355 ) ;
#197=CARTESIAN_POINT ( 'NONE',  ( 4.153883524164314167, 10.89765663934413276, -24.65439000785841372 ) ) ;
#205=CARTESIAN_POINT ( 'NONE',  ( 4.736559457325700606, 51.60997564292328121, 27.59650980994295466 ) ) ;
#207=DIRECTION ( 'NONE',  ( 1.000000000000000000, 0.000000000000000000, 0.000000000000000000 ) ) ;
#213=CARTESIAN_POINT ( 'NONE',  ( -4.680751350184292114, 48.23435024407273630, -27.60606166384445714 ) ) ;
#221=DIRECTION ( 'NONE',  ( 0.000000000000000000, 0.000000000000000000, -1.000000000000000000 ) ) ;
#235=EDGE_CURVE ( 'NONE', #3714, #6224, #3532, .T. ) ;
#240=PRODUCT_DEFINITION ( 'UNKNOWN', '', #9002, #6124 ) ;
#242=CARTESIAN_POINT ( 'NONE',  ( -1.002883791299520887E-19, 10.00000000000000000, -25.00000000000000000 ) ) ;
#247=CARTESIAN_POINT ( 'NONE',  ( 5.000000000000000000, 50.00000000000000000, -24.49489742783178414 ) ) ;
#250=CARTESIAN_POINT ( 'NONE',  ( -2.507472281498270394, 45.66193322363204032, 27.88882835875018174 ) ) ;
#269=CARTESIAN_POINT ( 'NONE',  ( 3.052391101563580733, 53.97379179909159319, 27.83448159811773692 ) ) ;
#275=CARTESIAN_POINT ( 'NONE',  ( -4.491894572514616435, 47.77948379856257333, -27.63764060679477552 ) ) ;
#292=VECTOR ( 'NONE', #10124, 1000.000000000000000 ) ;
#293=CARTESIAN_POINT ( 'NONE',  ( -3.303835886662602306, 53.76734242787640028, 27.80538831778189746 ) ) ;
#303=CIRCLE ( 'NONE', #9825, 28.00000000000000355 ) ;
#316=CARTESIAN_POINT ( 'NONE',  ( -5.302459511815778903, 11.51535060788542353, -27.49471880134667146 ) ) ;
#333=ADVANCED_FACE ( 'NONE', ( #11509 ), #1613, .T. ) ;
#338=CARTESIAN_POINT ( 'NONE',  ( -0.6576255085612114915, 54.96747678544938509, -27.99413849967543300 ) ) ;
#340=CARTESIAN_POINT ( 'NONE',  ( -2.643792293865090848, 45.75297423536069630, -27.87524183494957342 ) ) ;
#350=CARTESIAN_POINT ( 'NONE',  ( -9.869694407337590292, 21.64268126127443281, 26.20293780891199020 ) ) ;
#352=CARTESIAN_POINT ( 'NONE',  ( 1.312675767292145190, 10.06452048457374460, 27.97675868925955811 ) ) ;
#368=CARTESIAN_POINT ( 'NONE',  ( -8.122732253212674891, 14.15824396964088372, -23.64440389997412950 ) ) ;
#375=CARTESIAN_POINT ( 'NONE',  ( -10.00000000000000355, 20.00000000000000355, 26.15339366124404208 ) ) ;
#380=CARTESIAN_POINT ( 'NONE',  ( -2.221358530307614654, 54.49149874209361144, 24.90297606857491175 ) ) ;
#389=ORIENTED_EDGE ( 'NONE', *, *, #1938, .T. ) ;
#404=B_SPLINE_CURVE_WITH_KNOTS ( 'NONE', 3,
 ( #9767, #3861, #1078, #7863, #11791, #5958, #7672, #10766, #3097, #11540, #316, #7991, #3349, #6273, #9132, #6089, #8179, #1333, #4302, #3230, #4244, #5262, #2395, #10144, #3291, #10023, #5138, #440 ),
 .UNSPECIFIED., .F., .F.,
 ( 4, 2, 2, 2, 2, 2, 2, 2, 2, 2, 2, 2, 2, 4 ),
 ( 0.03152712852766463569, 0.03251194422550396368, 0.03349675992334329166, 0.03546639131902194764, 0.03645120701686126868, 0.03743602271470059667, 0.03940565411037925264, 0.04039046980821858063, 0.04137528550605790167, 0.04236010120389722966, 0.04334491690173655765, 0.04531454829741522056, 0.04629936399525454854, 0.04728417969309388347 ),
 .UNSPECIFIED. ) ;
#417=CARTESIAN_POINT ( 'NONE',  ( 9.355344799098423536, 23.54748521564438235, 26.39119804395479818 ) ) ;
#435=CARTESIAN_POINT ( 'NONE',  ( -10.00000000000000178, 19.67188320840964622, 26.15339366124404563 ) ) ;
#436=CARTESIAN_POINT ( 'NONE',  ( -3.049447146744188153, 46.02418402111927520, 27.83478105833641791 ) ) ;
#440=CARTESIAN_POINT ( 'NONE',  ( -10.00000000000000355, 20.00000000000000355, -26.15339366124404563 ) ) ;
#471=EDGE_CURVE ( 'NONE', #6633, #12230, #7168, .T. ) ;
#474=DIRECTION ( 'NONE',  ( 0.000000000000000000, 1.000000000000000000, 0.000000000000000000 ) ) ;
#479=CARTESIAN_POINT ( 'NONE',  ( 2.282621191639543134, 29.74158684310808098, 27.90868772972744694 ) ) ;
#493=CARTESIAN_POINT ( 'NONE',  ( 0.000000000000000000, 67.00000000000000000, -28.00000000000000000 ) ) ;
#502=CARTESIAN_POINT ( 'NONE',  ( 6.955575927950914131E-22, 45.00000000000000711, -25.00000000000000000 ) ) ;
#504=CARTESIAN_POINT ( 'NONE',  ( -4.246666789336575931, 52.64435674096336015, 24.63684932116156645 ) ) ;
#510=CARTESIAN_POINT ( 'NONE',  ( 10.00000000000000355, 20.00000000000000355, -22.91287847477919826 ) ) ;
#531=CARTESIAN_POINT ( 'NONE',  ( -7.536943458953863306, 26.60426427458575205, 26.97071265772227378 ) ) ;
#534=DIRECTION ( 'NONE',  ( -0.000000000000000000, -1.000000000000000000, -0.000000000000000000 ) ) ;
#540=DIRECTION ( 'NONE',  ( -0.000000000000000000, -1.000000000000000000, -0.000000000000000000 ) ) ;
#543=CARTESIAN_POINT ( 'NONE',  ( 4.339699721346885752, 52.50479725378321660, -24.62114839412567235 ) ) ;
#553=DIRECTION ( 'NONE',  ( -0.000000000000000000, -0.000000000000000000, 1.000000000000000000 ) ) ;
#557=B_SPLINE_CURVE_WITH_KNOTS ( 'NONE', 3,
 ( #1543, #12013, #5417, #4214, #5170, #11953, #3317, #11555, #9592, #2864, #4581, #835, #5483, #4516, #5664, #7500, #4703, #1602, #10409, #6599, #900, #11308, #3622, #10532 ),
 .UNSPECIFIED., .F., .F.,
 ( 4, 2, 2, 2, 2, 2, 2, 2, 2, 2, 2, 4 ),
 ( 0.04728417969309388347, 0.04925452359716459005, 0.05023969554919995029, 0.05122486750123530358, 0.05221003945327065687, 0.05319521140530601017, 0.05516555530937670981, 0.05713589921344740252, 0.05910624311751810217, 0.06009141506955345546, 0.06107658702158880182, 0.06304693092565949453 ),
 .UNSPECIFIED. ) ;
#575=DIRECTION ( 'NONE',  ( -0.000000000000000000, -1.000000000000000000, -0.000000000000000000 ) ) ;
#578=B_SPLINE_CURVE_WITH_KNOTS ( 'NONE', 3,
 ( #2023, #1152, #7096, #9774, #1084, #4949, #8813, #197, #3991, #11740, #6907, #6028, #7933, #9902, #9201, #5330, #12117, #12239, #6399, #6279, #8248, #1402, #8185, #2462, #3420, #510 ),
 .UNSPECIFIED., .F., .F.,
 ( 4, 2, 2, 2, 2, 2, 2, 2, 2, 2, 2, 2, 4 ),
 ( 0.03159890529972236156, 0.03258580175252957789, 0.03357269820533679422, 0.03554649111095121994, 0.03653338756375844321, 0.03752028401656565260, 0.03949407692218008525, 0.04146786982779451791, 0.04245476628060172730, 0.04344166273340894363, 0.04541545563902336935, 0.04640235209183058568, 0.04738924854463780201 ),
 .UNSPECIFIED. ) ;
#580=CARTESIAN_POINT ( 'NONE',  ( -4.339864767223333253, 52.50448352687625686, -27.66223537364948015 ) ) ;
#584=CARTESIAN_POINT ( 'NONE',  ( 9.916835782772588814, 21.32911185711201796, 22.94902338049798374 ) ) ;
#591=CARTESIAN_POINT ( 'NONE',  ( -5.033433411003701785, 28.66518080936452861, 27.54934970082421941 ) ) ;
#592=ORIENTED_EDGE ( 'NONE', *, *, #4345, .F. ) ;
#603=AXIS2_PLACEMENT_3D ( 'NONE', #10554, #4789, #8655 ) ;
#604=CARTESIAN_POINT ( 'NONE',  ( -4.493559251511619834, 47.78304274923282691, 24.59317321405577772 ) ) ;
#607=EDGE_LOOP ( 'NONE', ( #9363, #7842, #4031, #12501, #7877, #12339 ) ) ;
#612=EDGE_CURVE ( 'NONE', #2987, #6725, #1484, .T. ) ;
#630=CARTESIAN_POINT ( 'NONE',  ( 4.967390183827647299, 49.34301876381886132, 24.50161767623307441 ) ) ;
#651=CARTESIAN_POINT ( 'NONE',  ( 0.000000000000000000, 0.000000000000000000, -25.00000000000000000 ) ) ;
#711=LINE ( 'NONE', #651, #11144 ) ;
#714=DIRECTION ( 'NONE',  ( -0.000000000000000000, -1.000000000000000000, -0.000000000000000000 ) ) ;
#716=CARTESIAN_POINT ( 'NONE',  ( 8.484924050289805564, 25.30202893790023921, -23.51686326738786192 ) ) ;
#717=CARTESIAN_POINT ( 'NONE',  ( 10.00000000000000355, 20.00000000000000355, 26.15339366124404563 ) ) ;
#732=CARTESIAN_POINT ( 'NONE',  ( 5.340684424226280325E-17, 55.00000000000000000, -25.00000000000000000 ) ) ;
#748=DIRECTION ( 'NONE',  ( 0.000000000000000000, 1.000000000000000000, 0.000000000000000000 ) ) ;
#753=CARTESIAN_POINT ( 'NONE',  ( 1.298299055536097368, 45.16027954822755675, 24.96835849755778014 ) ) ;
#780=CARTESIAN_POINT ( 'NONE',  ( 3.429011037612589276E-15, 67.00000000000000000, 28.00000000000000000 ) ) ;
#795=CARTESIAN_POINT ( 'NONE',  ( -10.00000000000000178, 20.32878730486446273, 22.91287847477919826 ) ) ;
#796=EDGE_CURVE ( 'NONE', #11194, #12230, #5974, .T. ) ;
#806=ORIENTED_EDGE ( 'NONE', *, *, #2258, .F. ) ;
#815=CARTESIAN_POINT ( 'NONE',  ( 1.295138726946435170, 45.15964000046352567, 27.97186371880082234 ) ) ;
#835=CARTESIAN_POINT ( 'NONE',  ( -7.941295046835175953, 26.11247055527810446, -26.85294978034395186 ) ) ;
#839=CARTESIAN_POINT ( 'NONE',  ( 1.300460267930548142, 45.16099265032655552, -27.97162858364709592 ) ) ;
#842=CARTESIAN_POINT ( 'NONE',  ( -0.6518953824324608126, 45.03170992320611532, -27.99428315319153526 ) ) ;
#850=VERTEX_POINT ( 'NONE', #2034 ) ;
#860=ORIENTED_EDGE ( 'NONE', *, *, #4043, .T. ) ;
#873=EDGE_CURVE ( 'NONE', #2882, #5573, #4490, .T. ) ;
#882=ORIENTED_EDGE ( 'NONE', *, *, #9800, .T. ) ;
#900=CARTESIAN_POINT ( 'NONE',  ( -2.283355574799413201, 29.74132092790486581, -27.90859578342948666 ) ) ;
#902=CARTESIAN_POINT ( 'NONE',  ( 3.238656815135313671, 29.46670881375417395, -24.79134413122120151 ) ) ;
#922=CARTESIAN_POINT ( 'NONE',  ( -2.290944097510326571, 29.73958545346254922, -24.89690719708686828 ) ) ;
#925=CARTESIAN_POINT ( 'NONE',  ( -4.149932937002940747, 29.10413268181202184, 24.65505180927770112 ) ) ;
#948=CARTESIAN_POINT ( 'NONE',  ( 2.286402882168606432, 10.25929110584701931, 24.89734643733720176 ) ) ;
#967=CARTESIAN_POINT ( 'NONE',  ( 2.215581936987904843, 54.49413548860790257, 27.91383394955003183 ) ) ;
#983=ORIENTED_EDGE ( 'NONE', *, *, #3645, .F. ) ;
#992=CARTESIAN_POINT ( 'NONE',  ( -2.645127067179048996, 54.24614625768938225, 27.87511004317194718 ) ) ;
#993=CARTESIAN_POINT ( 'NONE',  ( 7.945602540532026303, 26.10722575314713723, -26.85169520992049996 ) ) ;
#1010=EDGE_CURVE ( 'NONE', #10421, #5573, #6897, .T. ) ;
#1012=DIRECTION ( 'NONE',  ( -0.000000000000000000, -1.000000000000000000, -0.000000000000000000 ) ) ;
#1014=DIRECTION ( 'NONE',  ( -0.000000000000000000, -1.000000000000000000, -0.000000000000000000 ) ) ;
#1018=CARTESIAN_POINT ( 'NONE',  ( 8.975091145622032585, 15.54177410167867990, 23.33498156074052687 ) ) ;
#1019=ORIENTED_EDGE ( 'NONE', *, *, #7656, .F. ) ;
#1031=ORIENTED_EDGE ( 'NONE', *, *, #873, .F. ) ;
#1051=CARTESIAN_POINT ( 'NONE',  ( -4.466051270639568749, 11.02833005318139925, 24.60558887372674519 ) ) ;
#1062=DIRECTION ( 'NONE',  ( -0.000000000000000000, -1.000000000000000000, -0.000000000000000000 ) ) ;
#1067=FACE_OUTER_BOUND ( 'NONE', #12430, .T. ) ;
#1068=CARTESIAN_POINT ( 'NONE',  ( 2.504881716134078395, 54.33965200799452333, 24.87570091612971979 ) ) ;
#1074=CARTESIAN_POINT ( 'NONE',  ( 4.838434350898961789, 48.69698515325892885, 27.57886596078574115 ) ) ;
#1078=CARTESIAN_POINT ( 'NONE',  ( -0.6564146843885075855, 10.01611589608920383, -27.99423190741217127 ) ) ;
#1084=CARTESIAN_POINT ( 'NONE',  ( 1.648701702613829090, 10.13131270077370338, -24.94769321807935825 ) ) ;
#1105=ORIENTED_EDGE ( 'NONE', *, *, #10705, .T. ) ;
#1107=EDGE_CURVE ( 'NONE', #3445, #2882, #3166, .T. ) ;
#1111=EDGE_LOOP ( 'NONE', ( #6272, #2199 ) ) ;
#1112=CARTESIAN_POINT ( 'NONE',  ( 8.979016783829413484, 15.54942851740142729, 26.52260613434120984 ) ) ;
#1121=CARTESIAN_POINT ( 'NONE',  ( 9.741722118349221304, 22.28203113172896366, -26.25078299423969952 ) ) ;
#1123=EDGE_LOOP ( 'NONE', ( #4739, #11937, #4393, #7054, #11382, #5372 ) ) ;
#1126=CARTESIAN_POINT ( 'NONE',  ( 0.000000000000000000, -3.000000000000003109, 0.000000000000000000 ) ) ;
#1142=CARTESIAN_POINT ( 'NONE',  ( 8.667518415056527203, 14.97026592263945410, 23.45254893740142066 ) ) ;
#1152=CARTESIAN_POINT ( 'NONE',  ( 0.3289161358670515400, 10.00000000000000355, -25.00000000000000711 ) ) ;
#1156=ORIENTED_EDGE ( 'NONE', *, *, #5948, .T. ) ;
#1171=AXIS2_PLACEMENT_3D ( 'NONE', #2713, #7729, #5763 ) ;
#1185=CARTESIAN_POINT ( 'NONE',  ( -2.505388173364745175, 54.33011157738807384, 27.88806253468715468 ) ) ;
#1194=CARTESIAN_POINT ( 'NONE',  ( -4.146974088394097535, 10.89458658634673327, -24.65552811365946440 ) ) ;
#1201=CARTESIAN_POINT ( 'NONE',  ( 2.644456282953588921, 45.75339465611970269, -24.86012065554512063 ) ) ;
#1204=CARTESIAN_POINT ( 'NONE',  ( -4.332262076698200737, 47.49833309567487305, 27.66292863318953366 ) ) ;
#1210=PRODUCT_CONTEXT ( 'NONE', #7562, 'mechanical' ) ;
#1231=EDGE_LOOP ( 'NONE', ( #11800, #2663, #6478, #8732 ) ) ;
#1233=CARTESIAN_POINT ( 'NONE',  ( -3.246935905771412667, 10.51876153604172970, 24.79592758899451255 ) ) ;
#1256=CARTESIAN_POINT ( 'NONE',  ( 2.217963917954424602, 54.49304390046189894, 24.90325875173717662 ) ) ;
#1258=DIRECTION ( 'NONE',  ( 0.000000000000000000, 0.000000000000000000, -1.000000000000000000 ) ) ;
#1267=CARTESIAN_POINT ( 'NONE',  ( -4.486434092443181143, 52.21331568334087336, 24.59426911350885092 ) ) ;
#1279=VERTEX_POINT ( 'NONE', #11653 ) ;
#1287=CARTESIAN_POINT ( 'NONE',  ( -1.619441697059012419, 54.74165912786163801, -27.95475164937197121 ) ) ;
#1326=CARTESIAN_POINT ( 'NONE',  ( -1.295685194009021490, 45.16801400859229432, 27.97044664692164773 ) ) ;
#1333=CARTESIAN_POINT ( 'NONE',  ( -8.488101409370928607, 14.70313273146787836, -26.68309740503542571 ) ) ;
#1344=EDGE_CURVE ( 'NONE', #9751, #10006, #4573, .T. ) ;
#1348=VERTEX_POINT ( 'NONE', #10624 ) ;
#1364=CARTESIAN_POINT ( 'NONE',  ( -10.00000000000000355, 20.00000000000000355, 26.15339366124404208 ) ) ;
#1366=CARTESIAN_POINT ( 'NONE',  ( 3.237495866348039986, 10.53285331842846340, 27.81400203867760368 ) ) ;
#1367=CARTESIAN_POINT ( 'NONE',  ( 4.999999999999999112, 49.67322169183177039, -27.54995462791183769 ) ) ;
#1368=DIRECTION ( 'NONE',  ( 0.000000000000000000, 0.000000000000000000, 1.000000000000000000 ) ) ;
#1372=CARTESIAN_POINT ( 'NONE',  ( 1.311921753209796648, 29.93550986204568787, 27.97677076635717341 ) ) ;
#1386=CYLINDRICAL_SURFACE ( 'NONE', #3731, 28.00000000000000355 ) ;
#1387=CARTESIAN_POINT ( 'NONE',  ( -9.869687208716547033, 18.35727153228636155, 26.20294053744295937 ) ) ;
#1389=CARTESIAN_POINT ( 'NONE',  ( -4.968290342600433007, 49.34811171367579163, 27.55576829111012316 ) ) ;
#1390=CARTESIAN_POINT ( 'NONE',  ( -0.6585108229100932187, 45.03273675766970285, -24.99339394906690970 ) ) ;
#1393=CARTESIAN_POINT ( 'NONE',  ( 3.061565168526138680E-15, 55.00000000000000000, 25.00000000000000000 ) ) ;
#1395=( GEOMETRIC_REPRESENTATION_CONTEXT ( 3 ) GLOBAL_UNCERTAINTY_ASSIGNED_CONTEXT ( ( #9754 ) ) GLOBAL_UNIT_ASSIGNED_CONTEXT ( ( #11010, #11965, #8161 ) ) REPRESENTATION_CONTEXT ( 'NONE', 'WORKASPACE' ) );
#1402=CARTESIAN_POINT ( 'NONE',  ( 9.868114579493717287, 18.34823788458374594, -22.97009550651098309 ) ) ;
#1415=CARTESIAN_POINT ( 'NONE',  ( -3.766645289650884632, 53.30424666614836582, -27.74645978028278392 ) ) ;
#1422=CARTESIAN_POINT ( 'NONE',  ( -9.673562854105167474, 17.38029584746389133, 23.05303382818504332 ) ) ;
#1443=ORIENTED_EDGE ( 'NONE', *, *, #5948, .F. ) ;
#1453=CARTESIAN_POINT ( 'NONE',  ( -4.245899883333350111, 47.35448134532762055, -24.63697916171703994 ) ) ;
#1478=CARTESIAN_POINT ( 'NONE',  ( -9.481487189274945493, 16.75591109918640242, 23.13382230614692148 ) ) ;
#1479=ORIENTED_EDGE ( 'NONE', *, *, #4810, .F. ) ;
#1484=LINE ( 'NONE', #10234, #11131 ) ;
#1489=CARTESIAN_POINT ( 'NONE',  ( 4.445126667670568743, 28.98136467921717241, 27.65156766125397070 ) ) ;
#1493=CARTESIAN_POINT ( 'NONE',  ( 5.000000000000000000, 50.00000000000000000, -24.49489742783178414 ) ) ;
#1513=AXIS2_PLACEMENT_3D ( 'NONE', #7542, #1014, #10511 ) ;
#1531=CARTESIAN_POINT ( 'NONE',  ( -5.000000000000000000, 50.00000000000000000, -27.54995462791182703 ) ) ;
#1537=CARTESIAN_POINT ( 'NONE',  ( 1.313665803496629980, 29.93556061881280428, 24.97400592093060112 ) ) ;
#1541=CARTESIAN_POINT ( 'NONE',  ( -7.945999201647152788, 13.89399703635140249, 23.70671076423498391 ) ) ;
#1543=CARTESIAN_POINT ( 'NONE',  ( -10.00000000000000355, 20.00000000000000355, -26.15339366124404563 ) ) ;
#1557=CARTESIAN_POINT ( 'NONE',  ( 0.000000000000000000, -3.000000000000003109, 0.000000000000000000 ) ) ;
#1563=DIRECTION ( 'NONE',  ( -0.000000000000000000, -1.000000000000000000, -0.000000000000000000 ) ) ;
#1564=VECTOR ( 'NONE', #2331, 1000.000000000000000 ) ;
#1581=CARTESIAN_POINT ( 'NONE',  ( 4.491750101222253377, 47.77928715861156661, 24.59350609687774281 ) ) ;
#1602=CARTESIAN_POINT ( 'NONE',  ( -3.543284028218923964, 29.35697078463959642, -27.77658592395861703 ) ) ;
#1613=CONICAL_SURFACE ( 'NONE', #603, 25.00000000000000355, 0.7853981633974482790 ) ;
#1640=CARTESIAN_POINT ( 'NONE',  ( 4.839779845606726916, 48.70264860999793655, 24.52714343409649089 ) ) ;
#1656=CARTESIAN_POINT ( 'NONE',  ( 8.972329510183547185, 24.46440230363330315, 23.33606587946024291 ) ) ;
#1662=CARTESIAN_POINT ( 'NONE',  ( 0.000000000000000000, 67.00000000000000000, 0.000000000000000000 ) ) ;
#1664=CARTESIAN_POINT ( 'NONE',  ( 5.839560020365381021, 28.12428960229776465, -24.30998564924267313 ) ) ;
#1665=CARTESIAN_POINT ( 'NONE',  ( 10.00000000000000533, 19.33329863329985443, 26.15339366124404563 ) ) ;
#1672=VERTEX_POINT ( 'NONE', #3461 ) ;
#1680=CARTESIAN_POINT ( 'NONE',  ( -7.930305867179300527, 26.10041404063223780, 23.70984975861344779 ) ) ;
#1684=CARTESIAN_POINT ( 'NONE',  ( 3.767132220643788720, 53.30373896185297866, -27.74639645793992671 ) ) ;
#1685=CARTESIAN_POINT ( 'NONE',  ( -1.648786683818842080, 10.13141593593141287, 27.95326983821354005 ) ) ;
#1699=CARTESIAN_POINT ( 'NONE',  ( 2.216120825188211185, 45.50613141711284015, 24.90340997055814398 ) ) ;
#1714=CARTESIAN_POINT ( 'NONE',  ( 8.124594680848492345, 25.83911103074633075, 23.64375881965231230 ) ) ;
#1725=CARTESIAN_POINT ( 'NONE',  ( 5.034037828167091000, 28.66467738801596354, -24.49412005228846922 ) ) ;
#1733=CARTESIAN_POINT ( 'NONE',  ( -3.051014581595654640, 46.02544827001062089, 24.81461801464184802 ) ) ;
#1736=CARTESIAN_POINT ( 'NONE',  ( 1.302929565828678582, 54.83844695853547790, -24.96811105270434439 ) ) ;
#1741=CARTESIAN_POINT ( 'NONE',  ( -9.868806730738530320, 21.64797418619996350, 22.96979908047426377 ) ) ;
#1748=VERTEX_POINT ( 'NONE', #6437 ) ;
#1759=CARTESIAN_POINT ( 'NONE',  ( 0.6550766687392827192, 45.03237040378185441, 27.99416758511093661 ) ) ;
#1800=CARTESIAN_POINT ( 'NONE',  ( -9.659227801817477754, 22.60918507870266581, -23.05884188866823337 ) ) ;
#1810=CARTESIAN_POINT ( 'NONE',  ( -4.147283247135973738, 10.89461892748662031, 27.69284716632408561 ) ) ;
#1824=CARTESIAN_POINT ( 'NONE',  ( 6.612460753110299017, 12.47060822435505756, 24.11434807139940517 ) ) ;
#1863=CARTESIAN_POINT ( 'NONE',  ( -5.845037936402837531, 28.12045204670673826, -24.30869324251348829 ) ) ;
#1865=CARTESIAN_POINT ( 'NONE',  ( -8.651571107376318182, 25.02565239439968536, 23.45586713013333124 ) ) ;
#1870=CARTESIAN_POINT ( 'NONE',  ( 3.973855183274129566, 53.05230689902806063, -27.71718999578467901 ) ) ;
#1872=CARTESIAN_POINT ( 'NONE',  ( -6.096819122263643642, 12.06690739318116812, 27.32937962794271414 ) ) ;
#1882=B_SPLINE_CURVE_WITH_KNOTS ( 'NONE', 3,
 ( #5809, #11646, #9682, #9872, #166, #2055, #4985, #1185, #992, #7964, #293, #7899, #6939, #3963, #6062, #11832, #3139, #4155, #2191, #8030 ),
 .UNSPECIFIED., .F., .F.,
 ( 4, 2, 2, 2, 2, 2, 2, 2, 2, 4 ),
 ( 0.007833747489473694495, 0.008812489889827121448, 0.009791232290180546666, 0.01028060349035726101, 0.01076997469053397535, 0.01174871709088740057, 0.01272745949124082926, 0.01370620189159425448, 0.01468494429194768143, 0.01566368669230110838 ),
 .UNSPECIFIED. ) ;
#1883=CYLINDRICAL_SURFACE ( 'NONE', #1171, 28.00000000000000355 ) ;
#1907=CARTESIAN_POINT ( 'NONE',  ( 9.983665987661890284, 19.33903170736681432, -26.15965704797978830 ) ) ;
#1915=DIRECTION ( 'NONE',  ( -0.000000000000000000, -0.000000000000000000, 1.000000000000000000 ) ) ;
#1929=CARTESIAN_POINT ( 'NONE',  ( 10.00000000000000355, 20.00000000000000355, 22.91287847477919826 ) ) ;
#1933=CARTESIAN_POINT ( 'NONE',  ( 10.00000000000000355, 20.00000000000000355, 26.15339366124404563 ) ) ;
#1938=EDGE_CURVE ( 'NONE', #1672, #3699, #10627, .T. ) ;
#1945=CARTESIAN_POINT ( 'NONE',  ( 0.000000000000000000, 0.000000000000000000, 0.000000000000000000 ) ) ;
#1947=CARTESIAN_POINT ( 'NONE',  ( 4.839602763736350788, 48.70207075804894714, -24.52717836283222752 ) ) ;
#1950=AXIS2_PLACEMENT_3D ( 'NONE', #5127, #9946, #7914 ) ;
#1953=CARTESIAN_POINT ( 'NONE',  ( 1.613533685434110465, 45.25622145510568828, 27.95510990066616941 ) ) ;
#1968=ORIENTED_EDGE ( 'NONE', *, *, #8089, .T. ) ;
#1969=CARTESIAN_POINT ( 'NONE',  ( 3.429011071898990822E-15, 55.00000000000000000, 28.00000000000000355 ) ) ;
#1983=VECTOR ( 'NONE', #10062, 1000.000000000000000 ) ;
#1986=CARTESIAN_POINT ( 'NONE',  ( -5.000000000000000000, 50.00000000000000000, -24.49489742783178059 ) ) ;
#2013=CARTESIAN_POINT ( 'NONE',  ( 3.048292328532992368, 46.02321945503342704, 27.83491629969137904 ) ) ;
#2023=CARTESIAN_POINT ( 'NONE',  ( -1.002883791299520887E-19, 10.00000000000000000, -25.00000000000000000 ) ) ;
#2034=CARTESIAN_POINT ( 'NONE',  ( 5.000000000000000000, 50.00000000000000000, -24.49489742783178414 ) ) ;
#2050=CARTESIAN_POINT ( 'NONE',  ( -9.355575343945487177, 23.54668771876638189, -23.18385937405269459 ) ) ;
#2055=CARTESIAN_POINT ( 'NONE',  ( -2.066793275460399926, 54.55579475875813245, 27.92402955534884512 ) ) ;
#2056=CARTESIAN_POINT ( 'NONE',  ( 9.357332009350985302, 23.54206009522648202, -26.39048829257603401 ) ) ;
#2064=MANIFOLD_SOLID_BREP ( 'Chamfer1', #11527 ) ;
#2077=ORIENTED_EDGE ( 'NONE', *, *, #5139, .T. ) ;
#2085=EDGE_CURVE ( 'NONE', #850, #4258, #4664, .T. ) ;
#2116=CARTESIAN_POINT ( 'NONE',  ( 9.661529737047111155, 17.39944252900632193, 26.28051061400176991 ) ) ;
#2117=CARTESIAN_POINT ( 'NONE',  ( -4.493909509445460415, 52.21603442804438799, -24.59310644668742540 ) ) ;
#2133=CARTESIAN_POINT ( 'NONE',  ( -1.643512924178977430, 10.13039013404520716, -24.94805769307042453 ) ) ;
#2136=PRODUCT_DEFINITION_SHAPE ( 'NONE', 'NONE',  #240 ) ;
#2163=CARTESIAN_POINT ( 'NONE',  ( 4.871799307858193373, 51.13674912335573453, 27.57293273687329105 ) ) ;
#2176=CARTESIAN_POINT ( 'NONE',  ( -10.00000000000000355, 20.00000000000000355, -28.00000000000000711 ) ) ;
#2183=CARTESIAN_POINT ( 'NONE',  ( 3.545294789778632882, 10.64386042719674919, 27.77630898643412394 ) ) ;
#2188=EDGE_CURVE ( 'NONE', #10800, #6113, #7, .T. ) ;
#2191=CARTESIAN_POINT ( 'NONE',  ( -5.000000000000000888, 50.32659431431049057, 27.54995462791181993 ) ) ;
#2194=AXIS2_PLACEMENT_3D ( 'NONE', #6493, #9485, #5678 ) ;
#2199=ORIENTED_EDGE ( 'NONE', *, *, #11568, .F. ) ;
#2221=B_SPLINE_CURVE_WITH_KNOTS ( 'NONE', 3,
 ( #2549, #7310, #2486, #10173, #9037, #2426, #2308, #9163, #591, #12200, #8086, #11241, #4331, #531, #5230, #8334, #3446, #6304, #3500, #6177, #4392, #350, #7184, #10053, #4271, #1364 ),
 .UNSPECIFIED., .F., .F.,
 ( 4, 2, 2, 2, 2, 2, 2, 2, 2, 2, 2, 2, 4 ),
 ( 0.01576777909941014244, 0.01675267178542435773, 0.01773756447143857301, 0.01970734984346701052, 0.02167713521549544456, 0.02266202790150966331, 0.02364692058752388554, 0.02561670595955232305, 0.02660159864556654180, 0.02758649133158076056, 0.02955627670360919113, 0.03054116938962340988, 0.03152606207563762863 ),
 .UNSPECIFIED. ) ;
#2258=EDGE_CURVE ( 'NONE', #1279, #2352, #4503, .T. ) ;
#2270=CARTESIAN_POINT ( 'NONE',  ( 4.491430111798321967, 52.22103771687890372, 24.59356092490497758 ) ) ;
#2278=CARTESIAN_POINT ( 'NONE',  ( -4.484481976314367735, 47.78274414339135490, -24.59462526944309246 ) ) ;
#2281=CARTESIAN_POINT ( 'NONE',  ( -1.614380680224908104, 54.74360302825979119, 24.94967786989446878 ) ) ;
#2295=AXIS2_PLACEMENT_3D ( 'NONE', #6970, #7929, #130 ) ;
#2299=CARTESIAN_POINT ( 'NONE',  ( -5.000000000000000000, 50.00000000000000000, -27.54995462791182703 ) ) ;
#2308=CARTESIAN_POINT ( 'NONE',  ( -3.240369384686552223, 29.48342856360252640, 27.81866359660341814 ) ) ;
#2319=CARTESIAN_POINT ( 'NONE',  ( 6.110050479722892725, 27.94346550729981971, 27.33088603378091008 ) ) ;
#2331=DIRECTION ( 'NONE',  ( 0.000000000000000000, -0.7071067811865479058, -0.7071067811865471286 ) ) ;
#2337=CARTESIAN_POINT ( 'NONE',  ( -0.3303383338888909448, 45.00000000000002132, 28.00000000000001066 ) ) ;
#2352=VERTEX_POINT ( 'NONE', #4269 ) ;
#2384=EDGE_CURVE ( 'NONE', #2615, #3714, #711, .T. ) ;
#2390=DIRECTION ( 'NONE',  ( 0.000000000000000000, 0.000000000000000000, -1.000000000000000000 ) ) ;
#2391=CARTESIAN_POINT ( 'NONE',  ( -9.483022228547349997, 16.75970615777680450, 26.34659568642391392 ) ) ;
#2395=CARTESIAN_POINT ( 'NONE',  ( -9.674976284561235929, 17.38768585986672122, -26.27572687994997835 ) ) ;
#2422=ORIENTED_EDGE ( 'NONE', *, *, #12202, .T. ) ;
#2425=ORIENTED_EDGE ( 'NONE', *, *, #235, .F. ) ;
#2426=CARTESIAN_POINT ( 'NONE',  ( -2.614082915411372721, 29.67457893774099986, 27.88517181684549229 ) ) ;
#2432=AXIS2_PLACEMENT_3D ( 'NONE', #6978, #10851, #9657 ) ;
#2445=CARTESIAN_POINT ( 'NONE',  ( 0.000000000000000000, 70.00000000000000000, 0.000000000000000000 ) ) ;
#2453=CARTESIAN_POINT ( 'NONE',  ( -8.964925771381055952, 15.55726866616962134, 26.52653170654884107 ) ) ;
#2462=CARTESIAN_POINT ( 'NONE',  ( 9.983753628317437290, 19.33993981085001579, -22.91999041428549688 ) ) ;
#2480=CARTESIAN_POINT ( 'NONE',  ( 6.112888882359681197, 27.94072674827362590, 24.24745615746033423 ) ) ;
#2486=CARTESIAN_POINT ( 'NONE',  ( -0.6612821460558259146, 29.98364310583667347, 27.99414546905236989 ) ) ;
#2514=CARTESIAN_POINT ( 'NONE',  ( 5.000000000000000000, 50.33107439471904598, 24.49489742783178770 ) ) ;
#2543=CARTESIAN_POINT ( 'NONE',  ( 9.867555937047535863, 21.65500574101911724, 22.97033549711487410 ) ) ;
#2545=ORIENTED_EDGE ( 'NONE', *, *, #11307, .F. ) ;
#2549=CARTESIAN_POINT ( 'NONE',  ( 3.429011038972528284E-15, 30.00000000000001066, 28.00000000000000355 ) ) ;
#2590=CARTESIAN_POINT ( 'NONE',  ( 1.614504882520976681, 45.25664461204844713, 24.94963714481321304 ) ) ;
#2615=VERTEX_POINT ( 'NONE', #5019 ) ;
#2619=B_SPLINE_CURVE_WITH_KNOTS ( 'NONE', 3,
 ( #1531, #3490, #12068, #6351, #5405, #9276, #580, #4446, #1415, #9977, #12190, #7361, #6108, #1287, #5160, #338, #4201, #3247 ),
 .UNSPECIFIED., .F., .F.,
 ( 4, 2, 2, 2, 2, 2, 2, 2, 4 ),
 ( 0.02349641915568531983, 0.02447480192481506570, 0.02545318469394481503, 0.02643156746307456090, 0.02740995023220430676, 0.02838833300133405610, 0.02936671577046380197, 0.03034509853959355130, 0.03132348130872329717 ),
 .UNSPECIFIED. ) ;
#2651=B_SPLINE_CURVE_WITH_KNOTS ( 'NONE', 3,
 ( #7651, #12410, #8727, #2764, #3588, #11584, #7462, #6693, #11457, #4861, #3649, #1684, #1870, #5813, #2828, #7527, #3841, #10561, #5752, #6626 ),
 .UNSPECIFIED., .F., .F.,
 ( 4, 2, 2, 2, 2, 2, 2, 2, 2, 4 ),
 ( 8.418992706677550310E-19, 0.0009792220048825109237, 0.001468833007323765844, 0.001958444009765020980, 0.002937666014647530820, 0.003916888019530041093, 0.004896110024412551366, 0.005875332029295060772, 0.006854554034177571045, 0.007833776039060080451 ),
 .UNSPECIFIED. ) ;
#2657=DIRECTION ( 'NONE',  ( -0.000000000000000000, -0.000000000000000000, 1.000000000000000000 ) ) ;
#2663=ORIENTED_EDGE ( 'NONE', *, *, #1938, .F. ) ;
#2671=CARTESIAN_POINT ( 'NONE',  ( 3.239919941357241040, 29.46629152487073000, 24.79118428027058840 ) ) ;
#2679=CARTESIAN_POINT ( 'NONE',  ( 0.3338900548043083893, 30.00000000000001066, -25.00000000000000355 ) ) ;
#2683=DIRECTION ( 'NONE',  ( 8.659560562354927928E-17, -0.7071067811865479058, 0.7071067811865471286 ) ) ;
#2687=CARTESIAN_POINT ( 'NONE',  ( -5.000000000000000000, 50.00000000000000000, 24.49489742783178414 ) ) ;
#2689=B_SPLINE_CURVE_WITH_KNOTS ( 'NONE', 3,
 ( #4156, #8385, #1537, #6128, #7492, #2671, #9218, #10339, #4385, #11902, #6415, #2480, #11234, #9281, #3208, #6534, #1714, #5537, #1656, #9998, #4574, #12315, #6356, #2543, #584, #11364, #4450, #8328 ),
 .UNSPECIFIED., .F., .F.,
 ( 4, 2, 2, 2, 2, 2, 2, 2, 2, 2, 2, 2, 2, 4 ),
 ( 0.04738593773884331589, 0.04935840384251231894, 0.05034463689434681699, 0.05133086994618132198, 0.05231710299801582004, 0.05330333604985031809, 0.05527580215351931420, 0.05626203520535381225, 0.05724826825718831030, 0.05922073436085731335, 0.06020696741269181834, 0.06119320046452632333, 0.06217943351636082833, 0.06316566656819533332 ),
 .UNSPECIFIED. ) ;
#2699=CARTESIAN_POINT ( 'NONE',  ( 3.061617454482527662E-15, 30.00000000000001066, 25.00000000000000000 ) ) ;
#2707=CONICAL_SURFACE ( 'NONE', #8996, 25.00000000000000355, 0.7853981633974482790 ) ;
#2710=ADVANCED_FACE ( 'NONE', ( #6913 ), #11682, .F. ) ;
#2713=CARTESIAN_POINT ( 'NONE',  ( 0.000000000000000000, 0.000000000000000000, 0.000000000000000000 ) ) ;
#2723=CARTESIAN_POINT ( 'NONE',  ( 3.429010155815331973E-15, 45.00000000000000711, 28.00000000000000355 ) ) ;
#2742=CARTESIAN_POINT ( 'NONE',  ( 4.967426332085672414, 50.65664594515786945, 27.55592256608452573 ) ) ;
#2744=DIRECTION ( 'NONE',  ( 0.000000000000000000, 0.000000000000000000, 1.000000000000000000 ) ) ;
#2746=CARTESIAN_POINT ( 'NONE',  ( 3.767400715871570327, 46.69623120791406734, -27.74638157013074391 ) ) ;
#2751=CARTESIAN_POINT ( 'NONE',  ( -4.999999999999999112, 49.67330453822126657, 24.49489742783177348 ) ) ;
#2758=CARTESIAN_POINT ( 'NONE',  ( -8.673894831530475358, 25.01911591053615425, -23.45021177788830968 ) ) ;
#2759=DIRECTION ( 'NONE',  ( -0.000000000000000000, -0.000000000000000000, 1.000000000000000000 ) ) ;
#2764=CARTESIAN_POINT ( 'NONE',  ( 1.136760544875492052, 54.87179675310391502, -27.97737333435675566 ) ) ;
#2765=DIRECTION ( 'NONE',  ( -0.000000000000000000, -0.000000000000000000, 1.000000000000000000 ) ) ;
#2777=CARTESIAN_POINT ( 'NONE',  ( 6.955575927950914131E-22, 45.00000000000000711, -25.00000000000000000 ) ) ;
#2779=CARTESIAN_POINT ( 'NONE',  ( 0.000000000000000000, 70.00000000000000000, -25.00000000000000000 ) ) ;
#2801=CARTESIAN_POINT ( 'NONE',  ( 4.462630933173456604, 28.97330998342967234, -24.60619142875309251 ) ) ;
#2815=CARTESIAN_POINT ( 'NONE',  ( 5.340684424226280325E-17, 55.00000000000000000, -25.00000000000000000 ) ) ;
#2816=ORIENTED_EDGE ( 'NONE', *, *, #9091, .T. ) ;
#2820=CARTESIAN_POINT ( 'NONE',  ( -7.533608174404544222, 26.60766787979761006, -23.84262432367340523 ) ) ;
#2823=CARTESIAN_POINT ( 'NONE',  ( -8.123193803314322281, 25.84109844632562769, 23.64424386314666648 ) ) ;
#2828=CARTESIAN_POINT ( 'NONE',  ( 4.494161248788206997, 52.21552753300132110, -27.63726652259117245 ) ) ;
#2841=CARTESIAN_POINT ( 'NONE',  ( 0.6521974589784806930, 45.03172573485493047, -24.99359419162020757 ) ) ;
#2864=CARTESIAN_POINT ( 'NONE',  ( -8.656972213103196978, 25.01632711531768294, -26.62861829799461333 ) ) ;
#2868=CARTESIAN_POINT ( 'NONE',  ( 8.976146624305494370, 15.54314380353506486, -26.52359378712270299 ) ) ;
#2882=VERTEX_POINT ( 'NONE', #2723 ) ;
#2883=CARTESIAN_POINT ( 'NONE',  ( -0.6685289520415670372, 30.00000000000001776, -25.00000000000001066 ) ) ;
#2896=DIRECTION ( 'NONE',  ( 0.000000000000000000, 1.000000000000000000, 0.000000000000000000 ) ) ;
#2927=CARTESIAN_POINT ( 'NONE',  ( 4.680557196582781465, 51.76613573486061171, 27.60609432111097306 ) ) ;
#2931=CARTESIAN_POINT ( 'NONE',  ( 7.516904306367743871, 13.39678444372546195, -26.97299697137856711 ) ) ;
#2944=B_SPLINE_CURVE_WITH_KNOTS ( 'NONE', 3,
 ( #5919, #9789, #842, #5673, #9544, #4261, #9092, #6230, #340, #8010, #7115, #4137, #8961, #6043, #275, #213, #7948, #5161, #10990, #11883, #6990, #2299 ),
 .UNSPECIFIED., .F., .F.,
 ( 4, 2, 2, 2, 2, 2, 2, 2, 2, 2, 4 ),
 ( 0.01566371915401241696, 0.01664280665422152028, 0.01762189415443062707, 0.01811143790453518393, 0.01860098165463973732, 0.01958006915484884758, 0.02055915665505796130, 0.02153824415526707156, 0.02202778790537162842, 0.02251733165547618529, 0.02349641915568531983 ),
 .UNSPECIFIED. ) ;
#2957=ORIENTED_EDGE ( 'NONE', *, *, #4665, .T. ) ;
#2985=CARTESIAN_POINT ( 'NONE',  ( 10.00000000000000355, 20.00000000000000355, -26.15339366124404208 ) ) ;
#2987=VERTEX_POINT ( 'NONE', #10450 ) ;
#2993=CARTESIAN_POINT ( 'NONE',  ( 3.239805147987244727, 10.51695055376340804, -27.81856429140262676 ) ) ;
#3001=ORIENTED_EDGE ( 'NONE', *, *, #4043, .F. ) ;
#3006=CARTESIAN_POINT ( 'NONE',  ( -4.461205683540790723, 28.97367431253432812, -24.60633856694852994 ) ) ;
#3015=ORIENTED_EDGE ( 'NONE', *, *, #5634, .T. ) ;
#3016=EDGE_CURVE ( 'NONE', #3699, #9751, #12185, .T. ) ;
#3027=CYLINDRICAL_SURFACE ( 'NONE', #1950, 5.000000000000000000 ) ;
#3028=CARTESIAN_POINT ( 'NONE',  ( 0.000000000000000000, 0.000000000000000000, -25.00000000000000000 ) ) ;
#3031=CARTESIAN_POINT ( 'NONE',  ( 3.061617023331388775E-15, 45.00000000000000711, 25.00000000000000000 ) ) ;
#3045=EDGE_CURVE ( 'NONE', #11194, #1279, #7509, .T. ) ;
#3053=CARTESIAN_POINT ( 'NONE',  ( 2.505714055585114508, 54.33929830399747374, 27.88900956191349678 ) ) ;
#3071=CARTESIAN_POINT ( 'NONE',  ( -4.968205859249467338, 50.65222807605660904, -24.50145347565533882 ) ) ;
#3082=ORIENTED_EDGE ( 'NONE', *, *, #12202, .F. ) ;
#3087=DIRECTION ( 'NONE',  ( 0.000000000000000000, 0.000000000000000000, -1.000000000000000000 ) ) ;
#3089=CARTESIAN_POINT ( 'NONE',  ( 4.743618752923510762, 48.38567045510036735, -24.54617134760821173 ) ) ;
#3097=CARTESIAN_POINT ( 'NONE',  ( -4.444287400701609769, 11.03583284713306689, -27.64660125085886122 ) ) ;
#3112=CARTESIAN_POINT ( 'NONE',  ( 4.492035651432232157, 52.22013966317427247, 27.63761663118750533 ) ) ;
#3116=CARTESIAN_POINT ( 'NONE',  ( 3.429010155815331973E-15, 45.00000000000000711, 28.00000000000000355 ) ) ;
#3126=ORIENTED_EDGE ( 'NONE', *, *, #8777, .F. ) ;
#3139=CARTESIAN_POINT ( 'NONE',  ( -4.839010323211785369, 51.30044682260506761, 27.57876396239285555 ) ) ;
#3140=CARTESIAN_POINT ( 'NONE',  ( 4.455554066248277323, 28.97648380245139066, -27.64996667850891754 ) ) ;
#3154=FACE_OUTER_BOUND ( 'NONE', #9605, .T. ) ;
#3158=CARTESIAN_POINT ( 'NONE',  ( 3.303834617765012194, 46.23291288788979614, -24.78182658752202983 ) ) ;
#3166=B_SPLINE_CURVE_WITH_KNOTS ( 'NONE', 3,
 ( #11982, #6085, #1389, #3288, #6018, #7149, #3225, #1204, #10900, #5071, #8937, #8051, #436, #250, #4106, #6143, #10018, #1326, #11025, #5197, #2337, #6206 ),
 .UNSPECIFIED., .F., .F.,
 ( 4, 2, 2, 2, 2, 2, 2, 2, 2, 2, 4 ),
 ( 0.01566368669230110838, 0.01664276945100601549, 0.01762185220971091912, 0.01811139358906338134, 0.01860093496841584357, 0.01958001772712077149, 0.02055910048582569594, 0.02153818324453062039, 0.02202772462388308261, 0.02251726600323554484, 0.02349634876194046582 ),
 .UNSPECIFIED. ) ;
#3167=CARTESIAN_POINT ( 'NONE',  ( -4.331872009808981794, 52.50234731214368367, 24.62196273622729592 ) ) ;
#3181=ORIENTED_EDGE ( 'NONE', *, *, #4811, .F. ) ;
#3193=ORIENTED_EDGE ( 'NONE', *, *, #11210, .F. ) ;
#3199=CARTESIAN_POINT ( 'NONE',  ( 7.950351283875114028, 13.89977645389732253, 26.85022583157104137 ) ) ;
#3208=CARTESIAN_POINT ( 'NONE',  ( 7.519126441075570710, 26.60062706338189642, 23.84344315696457173 ) ) ;
#3209=CARTESIAN_POINT ( 'NONE',  ( -0.3269774092232215490, 45.00000000000000000, 25.00000000000000711 ) ) ;
#3217=CARTESIAN_POINT ( 'NONE',  ( -6.110563603929655585, 12.05744620208248286, -24.24805373538051967 ) ) ;
#3220=CARTESIAN_POINT ( 'NONE',  ( 3.971273688083300613, 53.05572982463418441, 24.68326415769028159 ) ) ;
#3222=CARTESIAN_POINT ( 'NONE',  ( 5.000000000000000888, 49.66980702654861801, -24.49489742783178059 ) ) ;
#3225=CARTESIAN_POINT ( 'NONE',  ( -4.486710833798473352, 47.78725105462267209, 27.63829844907263222 ) ) ;
#3230=CARTESIAN_POINT ( 'NONE',  ( -8.964101468300798459, 15.55575854408322556, -26.52680384688584070 ) ) ;
#3247=CARTESIAN_POINT ( 'NONE',  ( -8.665812433443574132E-16, 55.00000000000000000, -28.00000000000000355 ) ) ;
#3248=EDGE_CURVE ( 'NONE', #8599, #850, #7151, .T. ) ;
#3272=AXIS2_PLACEMENT_3D ( 'NONE', #8318, #575, #12187 ) ;
#3273=EDGE_CURVE ( 'NONE', #8883, #2615, #4476, .T. ) ;
#3279=CARTESIAN_POINT ( 'NONE',  ( -6.608660176926854923, 12.46713484822145190, -24.11541629257941111 ) ) ;
#3287=CARTESIAN_POINT ( 'NONE',  ( 3.429011071898990822E-15, 55.00000000000000000, 28.00000000000000355 ) ) ;
#3288=CARTESIAN_POINT ( 'NONE',  ( -4.839543938134134748, 48.70089194556705792, 27.57867091635483447 ) ) ;
#3291=CARTESIAN_POINT ( 'NONE',  ( -9.917679487371039215, 18.67710825656768492, -26.18474513470922460 ) ) ;
#3296=LINE ( 'NONE', #9140, #8370 ) ;
#3315=CARTESIAN_POINT ( 'NONE',  ( -9.918789871757258680, 18.68607266337350836, 22.94817778295035993 ) ) ;
#3317=CARTESIAN_POINT ( 'NONE',  ( -9.356538917183957693, 23.54422275815007382, -26.39077148263137218 ) ) ;
#3332=CARTESIAN_POINT ( 'NONE',  ( 4.967652032308136789, 50.65502714036492904, -24.50156428836015721 ) ) ;
#3347=CARTESIAN_POINT ( 'NONE',  ( -1.301064515050044168, 45.16113941612564275, -24.96819193944210724 ) ) ;
#3349=CARTESIAN_POINT ( 'NONE',  ( -6.611445631918658528, 12.46901802506235413, -27.21243546183779216 ) ) ;
#3389=CARTESIAN_POINT ( 'NONE',  ( 10.00000000000000000, 20.66692791361947812, 26.15339366124403853 ) ) ;
#3397=VECTOR ( 'NONE', #6686, 1000.000000000000000 ) ;
#3400=CARTESIAN_POINT ( 'NONE',  ( 3.045782272221063902, 53.96862488584907425, 24.81409817615884705 ) ) ;
#3420=CARTESIAN_POINT ( 'NONE',  ( 10.00000000000000533, 19.67046583110989744, -22.91287847477920181 ) ) ;
#3445=VERTEX_POINT ( 'NONE', #7785 ) ;
#3446=CARTESIAN_POINT ( 'NONE',  ( -8.658590212363067806, 25.01362066216688262, 26.62809547983346548 ) ) ;
#3461=CARTESIAN_POINT ( 'NONE',  ( 0.000000000000000000, -3.000000000000003109, 25.00000000000000355 ) ) ;
#3490=CARTESIAN_POINT ( 'NONE',  ( -5.000000000000000000, 50.33010793893004831, -27.54995462791181993 ) ) ;
#3500=CARTESIAN_POINT ( 'NONE',  ( -9.108306422252258727, 24.14061933117464775, 26.47746754580360218 ) ) ;
#3527=CARTESIAN_POINT ( 'NONE',  ( -9.983890631919367209, 19.34374299500451855, 26.15957060131868417 ) ) ;
#3532=B_SPLINE_CURVE_WITH_KNOTS ( 'NONE', 3,
 ( #6811, #2883, #11701, #922, #4916, #12525, #3832, #3006, #5869, #1863, #7708, #6619, #10738, #2820, #11449, #2758, #10490, #2050, #5743, #1800, #6874, #10675, #5930, #8776 ),
 .UNSPECIFIED., .F., .F.,
 ( 4, 2, 2, 2, 2, 2, 2, 2, 2, 2, 2, 4 ),
 ( 5.438949063372056100E-19, 0.001975691086292785757, 0.002963536629439178418, 0.003951382172585572380, 0.005927073258878355969, 0.006914918802024747763, 0.007902764345171137822, 0.009878455431463928349, 0.01185414651775671888, 0.01284199206090311240, 0.01382983760404950767, 0.01580552869034228605 ),
 .UNSPECIFIED. ) ;
#3542=CARTESIAN_POINT ( 'NONE',  ( 4.743169864344128683, 48.38453593858750423, 24.54625634892152775 ) ) ;
#3546=CARTESIAN_POINT ( 'NONE',  ( 10.00000000000000533, 19.33140358361892552, 22.91287847477920891 ) ) ;
#3561=ORIENTED_EDGE ( 'NONE', *, *, #10397, .T. ) ;
#3583=B_SPLINE_CURVE_WITH_KNOTS ( 'NONE', 3,
 ( #9070, #9195, #10082, #11090, #5324, #6210, #1267, #3167, #504, #7091, #8943, #9962, #4180, #10973, #380, #2281, #8057, #6149, #11986, #1393 ),
 .UNSPECIFIED., .F., .F.,
 ( 4, 2, 2, 2, 2, 2, 2, 2, 2, 4 ),
 ( 0.01567180661725443153, 0.01665134708417310289, 0.01763088755109177425, 0.01812065778455110993, 0.01861042801801044561, 0.01958996848492911697, 0.02056950895184778833, 0.02154904941876645622, 0.02252858988568512758, 0.02350813035260379893 ),
 .UNSPECIFIED. ) ;
#3588=CARTESIAN_POINT ( 'NONE',  ( 1.295434377910737567, 54.83206668271250805, -27.97046038954552216 ) ) ;
#3591=AXIS2_PLACEMENT_3D ( 'NONE', #4559, #2657, #5581 ) ;
#3596=FACE_OUTER_BOUND ( 'NONE', #10423, .T. ) ;
#3601=CARTESIAN_POINT ( 'NONE',  ( 0.6522419138580031195, 45.03179559853693092, 24.99358091562669060 ) ) ;
#3605=CARTESIAN_POINT ( 'NONE',  ( 3.061616997868383437E-15, -3.000000000000003109, -25.00000000000000355 ) ) ;
#3609=AXIS2_PLACEMENT_3D ( 'NONE', #10825, #8933, #1258 ) ;
#3622=CARTESIAN_POINT ( 'NONE',  ( -0.6666273477411399639, 30.00000000000001421, -28.00000000000000355 ) ) ;
#3643=CARTESIAN_POINT ( 'NONE',  ( -0.6569842770428546697, 54.96739046863824996, -24.99342020365237360 ) ) ;
#3645=EDGE_CURVE ( 'NONE', #6159, #10270, #2221, .T. ) ;
#3649=CARTESIAN_POINT ( 'NONE',  ( 3.306945158608051827, 53.76431800115727100, -27.80499802709851664 ) ) ;
#3652=DIRECTION ( 'NONE',  ( 0.000000000000000000, 0.000000000000000000, -1.000000000000000000 ) ) ;
#3662=EDGE_CURVE ( 'NONE', #5412, #10229, #557, .T. ) ;
#3667=FACE_OUTER_BOUND ( 'NONE', #7123, .T. ) ;
#3682=DIRECTION ( 'NONE',  ( -0.000000000000000000, -1.000000000000000000, -0.000000000000000000 ) ) ;
#3684=CARTESIAN_POINT ( 'NONE',  ( 5.000000000000000000, 50.00000000000000000, 27.54995462791182703 ) ) ;
#3699=VERTEX_POINT ( 'NONE', #4770 ) ;
#3714=VERTEX_POINT ( 'NONE', #5543 ) ;
#3727=DIRECTION ( 'NONE',  ( 8.659560562354932858E-17, 0.7071067811865474617, -0.7071067811865474617 ) ) ;
#3731=AXIS2_PLACEMENT_3D ( 'NONE', #9126, #11085, #2390 ) ;
#3735=ADVANCED_FACE ( 'NONE', ( #5602 ), #3868, .T. ) ;
#3747=CARTESIAN_POINT ( 'NONE',  ( 9.104442389086463194, 24.14915179589751304, -23.28362858151144721 ) ) ;
#3753=AXIS2_PLACEMENT_3D ( 'NONE', #5880, #2896, #3652 ) ;
#3765=EDGE_CURVE ( 'NONE', #5573, #6725, #10838, .T. ) ;
#3779=ORIENTED_EDGE ( 'NONE', *, *, #11307, .T. ) ;
#3784=LINE ( 'NONE', #12360, #9881 ) ;
#3792=CARTESIAN_POINT ( 'NONE',  ( 2.217624749121678729, 45.50677551093724560, 27.91368483350839824 ) ) ;
#3816=CARTESIAN_POINT ( 'NONE',  ( 2.615458182459051706, 10.32545218288117717, -27.88515796981556960 ) ) ;
#3818=LINE ( 'NONE', #780, #12236 ) ;
#3827=CARTESIAN_POINT ( 'NONE',  ( 0.6578411763953998515, 54.96743791211429908, -24.99342793576595767 ) ) ;
#3832=CARTESIAN_POINT ( 'NONE',  ( -3.554546826686217020, 29.35267307038308360, -24.74790415999775917 ) ) ;
#3841=CARTESIAN_POINT ( 'NONE',  ( 4.839828837987002252, 51.29788161226999677, -27.57862052135422459 ) ) ;
#3849=LINE ( 'NONE', #7789, #5403 ) ;
#3858=CARTESIAN_POINT ( 'NONE',  ( 7.297088297540795132, 13.15481214220262274, 23.91253034306283354 ) ) ;
#3859=VERTEX_POINT ( 'NONE', #10592 ) ;
#3861=CARTESIAN_POINT ( 'NONE',  ( -0.3281837927571703561, 10.00000000000000711, -28.00000000000001066 ) ) ;
#3868=CONICAL_SURFACE ( 'NONE', #4680, 28.00000000000000000, 0.7853981633974477239 ) ;
#3870=ORIENTED_EDGE ( 'NONE', *, *, #11183, .T. ) ;
#3899=CARTESIAN_POINT ( 'NONE',  ( 6.608094568897072030, 27.51261231993640166, -27.21028944860474397 ) ) ;
#3915=CARTESIAN_POINT ( 'NONE',  ( -10.00000000000000355, 20.00000000000000355, -26.15339366124404563 ) ) ;
#3919=CARTESIAN_POINT ( 'NONE',  ( 5.000000000000000000, 50.00000000000000000, 27.54995462791182703 ) ) ;
#3934=ORIENTED_EDGE ( 'NONE', *, *, #2384, .F. ) ;
#3938=CARTESIAN_POINT ( 'NONE',  ( 0.3269428999352006482, 55.00000000000000711, 28.00000000000000711 ) ) ;
#3955=CARTESIAN_POINT ( 'NONE',  ( -2.618974170005213153, 10.32668121623932400, 24.87084347637328108 ) ) ;
#3963=CARTESIAN_POINT ( 'NONE',  ( -4.336936024885986285, 52.50935177099758278, 27.66269046005032095 ) ) ;
#3969=ORIENTED_EDGE ( 'NONE', *, *, #11568, .T. ) ;
#3987=AXIS2_PLACEMENT_3D ( 'NONE', #10570, #748, #8488 ) ;
#3991=CARTESIAN_POINT ( 'NONE',  ( 4.452539714567801177, 11.03997247681473404, -24.60205477162727661 ) ) ;
#3999=CARTESIAN_POINT ( 'NONE',  ( 3.303823242547402117, 53.76705800516405276, 27.80537070972012259 ) ) ;
#4000=ORIENTED_EDGE ( 'NONE', *, *, #3765, .F. ) ;
#4010=FACE_OUTER_BOUND ( 'NONE', #1123, .T. ) ;
#4017=MECHANICAL_DESIGN_GEOMETRIC_PRESENTATION_REPRESENTATION('',(#9498),#1395);
#4018=CARTESIAN_POINT ( 'NONE',  ( 4.442227524869980293, 11.03487569001018009, 27.64691637681915282 ) ) ;
#4021=AXIS2_PLACEMENT_3D ( 'NONE', #9450, #5706, #7539 ) ;
#4026=CARTESIAN_POINT ( 'NONE',  ( 3.236409131694046426, 29.46755692282902928, -27.81414090612697976 ) ) ;
#4031=ORIENTED_EDGE ( 'NONE', *, *, #1107, .T. ) ;
#4043=EDGE_CURVE ( 'NONE', #3859, #2987, #29, .T. ) ;
#4066=CARTESIAN_POINT ( 'NONE',  ( 9.674670850494081265, 17.38628865587025984, -26.27584064538169173 ) ) ;
#4075=ORIENTED_EDGE ( 'NONE', *, *, #67, .T. ) ;
#4083=CARTESIAN_POINT ( 'NONE',  ( -3.973726775714538029, 53.05247132632594287, -24.68286527305685141 ) ) ;
#4088=LINE ( 'NONE', #5051, #7172 ) ;
#4089=CARTESIAN_POINT ( 'NONE',  ( 9.935543424393982193, 21.31157940332991174, -26.17831177576534785 ) ) ;
#4094=ORIENTED_EDGE ( 'NONE', *, *, #612, .F. ) ;
#4097=DIRECTION ( 'NONE',  ( 0.000000000000000000, 0.7071067811865474617, 0.7071067811865474617 ) ) ;
#4100=CARTESIAN_POINT ( 'NONE',  ( 0.3299754220453550713, 55.00000000000001421, 25.00000000000000000 ) ) ;
#4106=CARTESIAN_POINT ( 'NONE',  ( -2.220574438802248807, 45.50813311347688739, 27.91346354743601310 ) ) ;
#4110=CARTESIAN_POINT ( 'NONE',  ( -2.509809017951089682, 45.66333224303983229, -24.87518608377025231 ) ) ;
#4137=CARTESIAN_POINT ( 'NONE',  ( -3.764971525938848540, 46.69375435830438192, -27.74669386146050698 ) ) ;
#4149=CARTESIAN_POINT ( 'NONE',  ( 5.300979503027939188, 11.51433960415130997, 27.49502322044257241 ) ) ;
#4150=CARTESIAN_POINT ( 'NONE',  ( -4.839726511208201742, 51.29827509403275343, -24.52715513826036897 ) ) ;
#4155=CARTESIAN_POINT ( 'NONE',  ( -4.967267959664427579, 50.65835542335811681, 27.55595201800184313 ) ) ;
#4156=CARTESIAN_POINT ( 'NONE',  ( 3.061617454482527662E-15, 30.00000000000001066, 25.00000000000000000 ) ) ;
#4163=VECTOR ( 'NONE', #1012, 1000.000000000000000 ) ;
#4180=CARTESIAN_POINT ( 'NONE',  ( -3.049660161009143611, 53.97562969122508747, 24.81478968795947537 ) ) ;
#4195=ORIENTED_EDGE ( 'NONE', *, *, #12508, .F. ) ;
#4197=AXIS2_PLACEMENT_3D ( 'NONE', #1945, #11661, #3087 ) ;
#4201=CARTESIAN_POINT ( 'NONE',  ( -0.3308735998258449107, 55.00000000000001421, -28.00000000000001066 ) ) ;
#4214=CARTESIAN_POINT ( 'NONE',  ( -9.741195869257412099, 22.28434334298316699, -26.25097870757294416 ) ) ;
#4216=CARTESIAN_POINT ( 'NONE',  ( 2.284872756015303707, 10.25892335484974538, 27.90850932234814152 ) ) ;
#4222=CARTESIAN_POINT ( 'NONE',  ( 9.467847366638277862, 23.23554191946201897, 26.35090841722655952 ) ) ;
#4231=CARTESIAN_POINT ( 'NONE',  ( -0.3289793214801078336, 10.00000000000000000, -25.00000000000000355 ) ) ;
#4235=CARTESIAN_POINT ( 'NONE',  ( 4.838449599032471404, 51.30291823734444989, 24.52740775798701378 ) ) ;
#4241=CARTESIAN_POINT ( 'NONE',  ( -3.302172444309792620, 46.23123523635531740, -24.78206517003335208 ) ) ;
#4244=CARTESIAN_POINT ( 'NONE',  ( -9.106140955794129965, 15.85440612518673476, -26.47821835386478284 ) ) ;
#4255=ORIENTED_EDGE ( 'NONE', *, *, #5368, .F. ) ;
#4258=VERTEX_POINT ( 'NONE', #12306 ) ;
#4261=CARTESIAN_POINT ( 'NONE',  ( -2.065290181436918893, 45.44356257902996532, -27.92413535551499848 ) ) ;
#4269=CARTESIAN_POINT ( 'NONE',  ( -10.00000000000000355, 20.00000000000000355, 22.91287847477919826 ) ) ;
#4271=CARTESIAN_POINT ( 'NONE',  ( -10.00000000000000533, 20.32816415950047073, 26.15339366124404208 ) ) ;
#4289=CARTESIAN_POINT ( 'NONE',  ( -4.441326820874226478, 11.03441940688963108, -24.60408056175351987 ) ) ;
#4298=CARTESIAN_POINT ( 'NONE',  ( -8.486085304528891982, 14.69985328301606842, 26.68374292945578574 ) ) ;
#4302=CARTESIAN_POINT ( 'NONE',  ( -8.655424981280289032, 14.98103440478909398, -26.62912044845977988 ) ) ;
#4315=B_SPLINE_CURVE_WITH_KNOTS ( 'NONE', 3,
 ( #5302, #3389, #7132, #10946, #9172, #4222, #417, #11006, #4464, #10240, #6314, #8279, #8343, #6374, #2319, #6186, #1489, #10061, #12148, #10181, #479, #1372, #5365, #4346 ),
 .UNSPECIFIED., .F., .F.,
 ( 4, 2, 2, 2, 2, 2, 2, 2, 2, 2, 2, 4 ),
 ( 0.000000000000000000, 0.001970972387426263902, 0.002956458581139390866, 0.003941944774852517396, 0.005912917162278783466, 0.006898403355991919103, 0.007883889549705055608, 0.009854861937131328617, 0.01182583432455759989, 0.01281132051827073466, 0.01379680671198387117, 0.01576777909941014244 ),
 .UNSPECIFIED. ) ;
#4331=CARTESIAN_POINT ( 'NONE',  ( -6.848757607247366153, 27.29383130221564713, 27.15051995320520462 ) ) ;
#4333=ORIENTED_EDGE ( 'NONE', *, *, #12357, .F. ) ;
#4339=SHAPE_REPRESENTATION ( 'Bolt-Mounted Retaining Cylinder', ( #9021 ), #5775 ) ;
#4345=EDGE_CURVE ( 'NONE', #1748, #5412, #404, .T. ) ;
#4346=CARTESIAN_POINT ( 'NONE',  ( 3.429011038972528284E-15, 30.00000000000001066, 28.00000000000000355 ) ) ;
#4347=DIRECTION ( 'NONE',  ( 0.000000000000000000, 0.000000000000000000, -1.000000000000000000 ) ) ;
#4348=ORIENTED_EDGE ( 'NONE', *, *, #4417, .F. ) ;
#4385=CARTESIAN_POINT ( 'NONE',  ( 4.444397983376138228, 28.96407317687630822, 24.60352964329958070 ) ) ;
#4392=CARTESIAN_POINT ( 'NONE',  ( -9.674652806887369394, 22.61498962668658308, 26.27585132995591621 ) ) ;
#4393=ORIENTED_EDGE ( 'NONE', *, *, #6827, .T. ) ;
#4417=EDGE_CURVE ( 'NONE', #11047, #6436, #3583, .T. ) ;
#4419=CARTESIAN_POINT ( 'NONE',  ( -6.597987972726388151, 12.47858281773167199, 27.21273137650036134 ) ) ;
#4446=CARTESIAN_POINT ( 'NONE',  ( -3.976827824928235611, 53.04822971330205661, -27.71675544712706696 ) ) ;
#4450=CARTESIAN_POINT ( 'NONE',  ( 10.00000000000000888, 20.33378987232122981, 22.91287847477920536 ) ) ;
#4464=CARTESIAN_POINT ( 'NONE',  ( 8.669775631709102370, 25.02591811617444151, 26.62666687084030315 ) ) ;
#4465=CARTESIAN_POINT ( 'NONE',  ( -4.838865259365938698, 48.69895664399926005, 24.52732495089485099 ) ) ;
#4468=CARTESIAN_POINT ( 'NONE',  ( 3.651743720672741667, 53.41923203171982237, -24.73212923346887848 ) ) ;
#4476=B_SPLINE_CURVE_WITH_KNOTS ( 'NONE', 3,
 ( #12047, #8054, #6147, #7089, #10831, #11028, #2278, #9893, #1453, #8240, #9068, #4241, #7989, #4110, #11983, #6208, #3347, #1390, #7214, #502 ),
 .UNSPECIFIED., .F., .F.,
 ( 4, 2, 2, 2, 2, 2, 2, 2, 2, 4 ),
 ( 0.007837888240810860288, 0.008817134455640363022, 0.009796380670469867491, 0.01028600377788460932, 0.01077562688529935114, 0.01175487310012885388, 0.01273411931495835661, 0.01371336552978785761, 0.01469261174461736208, 0.01567185795944686308 ),
 .UNSPECIFIED. ) ;
#4490=B_SPLINE_CURVE_WITH_KNOTS ( 'NONE', 3,
 ( #3116, #10856, #1759, #815, #1953, #3792, #7795, #2013, #5642, #8617, #9575, #122, #11599, #10513, #1074, #11667, #11472, #3919 ),
 .UNSPECIFIED., .F., .F.,
 ( 4, 2, 2, 2, 2, 2, 2, 2, 4 ),
 ( 0.02349634876194046582, 0.02447473093966404806, 0.02545311311738762683, 0.02643149529511120907, 0.02740987747283479131, 0.02838825965055837355, 0.02936664182828195579, 0.03034502400600553804, 0.03132340618372912028 ),
 .UNSPECIFIED. ) ;
#4495=CARTESIAN_POINT ( 'NONE',  ( 3.052604782738682854, 46.02637368922790984, 24.81445626415020200 ) ) ;
#4503=B_SPLINE_CURVE_WITH_KNOTS ( 'NONE', 3,
 ( #8903, #10867, #9735, #6051, #9924, #3955, #1233, #1051, #7829, #6301, #11118, #10111, #10171, #12075, #1541, #5228, #8207, #11951, #11181, #1478, #1422, #5168, #3315, #12011, #6237, #6361 ),
 .UNSPECIFIED., .F., .F.,
 ( 4, 2, 2, 2, 2, 2, 2, 2, 2, 2, 2, 2, 4 ),
 ( 0.01580376012220196039, 0.01679085241551835084, 0.01777794470883474129, 0.01975212929546752219, 0.02172631388210030656, 0.02271340617541669701, 0.02370049846873308746, 0.02567468305536586837, 0.02666177534868225882, 0.02764886764199864927, 0.02962305222863143364, 0.03061014452194782409, 0.03159723681526421801 ),
 .UNSPECIFIED. ) ;
#4516=CARTESIAN_POINT ( 'NONE',  ( -6.613224532456894345, 27.52898668827616646, -27.21194102765744560 ) ) ;
#4520=CARTESIAN_POINT ( 'NONE',  ( 6.844556472468130259, 27.29775667647069071, -24.04598060202682319 ) ) ;
#4535=ORIENTED_EDGE ( 'NONE', *, *, #11233, .F. ) ;
#4559=CARTESIAN_POINT ( 'NONE',  ( 0.000000000000000000, 50.00000000000000000, -28.00000000000000711 ) ) ;
#4573=CIRCLE ( 'NONE', #3753, 28.00000000000000355 ) ;
#4574=CARTESIAN_POINT ( 'NONE',  ( 9.465308527890080370, 23.24274166418333110, 23.13911695433847981 ) ) ;
#4581=CARTESIAN_POINT ( 'NONE',  ( -8.486922698271502696, 25.29893941662590251, -26.68348577013889056 ) ) ;
#4586=CARTESIAN_POINT ( 'NONE',  ( 0.3265943374146230704, 45.00000000000000711, -28.00000000000000000 ) ) ;
#4593=CARTESIAN_POINT ( 'NONE',  ( -3.768871583585197360, 46.69794849765531808, 24.71539284385418611 ) ) ;
#4614=DIRECTION ( 'NONE',  ( -0.000000000000000000, -1.000000000000000000, -0.000000000000000000 ) ) ;
#4622=AXIS2_PLACEMENT_3D ( 'NONE', #1557, #540, #4347 ) ;
#4654=CARTESIAN_POINT ( 'NONE',  ( -2.645619823791141467, 45.75416279094086036, 24.85999165416970413 ) ) ;
#4664=B_SPLINE_CURVE_WITH_KNOTS ( 'NONE', 3,
 ( #1493, #12028, #3332, #5370, #9240, #9302, #543, #8284, #7324, #7387, #4468, #7514, #7451, #6615, #8467, #6679, #1736, #3827, #5681, #2815 ),
 .UNSPECIFIED., .F., .F.,
 ( 4, 2, 2, 2, 2, 2, 2, 2, 2, 4 ),
 ( 0.02350824016915415912, 0.02448716854195917558, 0.02546609691476419204, 0.02644502528756920851, 0.02693448947397171500, 0.02742395366037422497, 0.02840288203317925531, 0.02938181040598428218, 0.03036073877878931251, 0.03133966715159434285 ),
 .UNSPECIFIED. ) ;
#4665=EDGE_CURVE ( 'NONE', #11427, #10229, #7194, .T. ) ;
#4666=CARTESIAN_POINT ( 'NONE',  ( -9.918452521082530282, 21.31677563331469116, 22.94832388515032662 ) ) ;
#4669=VERTEX_POINT ( 'NONE', #11071 ) ;
#4673=CARTESIAN_POINT ( 'NONE',  ( -3.237458362839043868, 10.51577337999971640, 27.81894738099048325 ) ) ;
#4678=ORIENTED_EDGE ( 'NONE', *, *, #3662, .F. ) ;
#4680=AXIS2_PLACEMENT_3D ( 'NONE', #1662, #714, #12321 ) ;
#4703=CARTESIAN_POINT ( 'NONE',  ( -4.452344947754465210, 28.97817800798833332, -27.65051488940038737 ) ) ;
#4705=CARTESIAN_POINT ( 'NONE',  ( 9.355409448593292154, 23.54720254436722371, -23.18392859692124830 ) ) ;
#4714=CYLINDRICAL_SURFACE ( 'NONE', #2194, 10.00000000000000355 ) ;
#4729=PLANE ( 'NONE',  #11330 ) ;
#4739=ORIENTED_EDGE ( 'NONE', *, *, #2258, .T. ) ;
#4762=B_SPLINE_CURVE_WITH_KNOTS ( 'NONE', 3,
 ( #6954, #4100, #8863, #9948, #9759, #1256, #1068, #7979, #3400, #6261, #8231, #11976, #3220, #11081, #2270, #5251, #4235, #9312, #2514, #7271 ),
 .UNSPECIFIED., .F., .F.,
 ( 4, 2, 2, 2, 2, 2, 2, 2, 2, 4 ),
 ( 0.02350813035260379893, 0.02448705762280033518, 0.02546598489299686796, 0.02644491216319340421, 0.02693437579829167233, 0.02742383943338994046, 0.02840276670358647670, 0.02938169397378300948, 0.03036062124397954226, 0.03133954851417607851 ),
 .UNSPECIFIED. ) ;
#4770=CARTESIAN_POINT ( 'NONE',  ( 3.245314017740486554E-15, -3.000000000000003109, -25.00000000000000355 ) ) ;
#4772=CARTESIAN_POINT ( 'NONE',  ( 1.651856453710261352, 29.86806670974593914, -24.94744891504881679 ) ) ;
#4789=DIRECTION ( 'NONE',  ( 0.000000000000000000, 1.000000000000000000, 0.000000000000000000 ) ) ;
#4810=EDGE_CURVE ( 'NONE', #3699, #1672, #5643, .T. ) ;
#4811=EDGE_CURVE ( 'NONE', #6575, #11047, #5390, .T. ) ;
#4815=DIRECTION ( 'NONE',  ( 1.000000000000000000, 0.000000000000000000, 0.000000000000000000 ) ) ;
#4844=CYLINDRICAL_SURFACE ( 'NONE', #6648, 10.00000000000000355 ) ;
#4854=CARTESIAN_POINT ( 'NONE',  ( -5.303430480311382311, 28.48399989248413178, 24.43255084236253794 ) ) ;
#4858=CARTESIAN_POINT ( 'NONE',  ( -4.140053538423851224E-16, 30.00000000000001066, -28.00000000000000355 ) ) ;
#4861=CARTESIAN_POINT ( 'NONE',  ( 3.050334177726442775, 53.97519422362026376, -27.83468959413792732 ) ) ;
#4864=ORIENTED_EDGE ( 'NONE', *, *, #6827, .F. ) ;
#4871=AXIS2_PLACEMENT_3D ( 'NONE', #8773, #11759, #221 ) ;
#4872=CARTESIAN_POINT ( 'NONE',  ( -5.000000000000000000, 50.00000000000000000, -28.00000000000000711 ) ) ;
#4876=CARTESIAN_POINT ( 'NONE',  ( -8.665812433443574132E-16, 55.00000000000000000, -28.00000000000000355 ) ) ;
#4893=ORIENTED_EDGE ( 'NONE', *, *, #5139, .F. ) ;
#4914=ADVANCED_FACE ( 'NONE', ( #7511 ), #4714, .F. ) ;
#4916=CARTESIAN_POINT ( 'NONE',  ( -2.610103423518925769, 29.65902056345734650, -24.86541183722168213 ) ) ;
#4917=CARTESIAN_POINT ( 'NONE',  ( -4.743369866101525112, 51.61445767325203349, -24.54621253249761637 ) ) ;
#4926=ORIENTED_EDGE ( 'NONE', *, *, #8399, .F. ) ;
#4949=CARTESIAN_POINT ( 'NONE',  ( 2.620611987601386250, 10.32688167823381953, -24.87076294850758984 ) ) ;
#4952=CARTESIAN_POINT ( 'NONE',  ( 3.061616997868383043E-15, 0.000000000000000000, 25.00000000000000000 ) ) ;
#4962=CARTESIAN_POINT ( 'NONE',  ( 9.917745391744515970, 18.67758101133046722, -26.18472015824584531 ) ) ;
#4981=DIRECTION ( 'NONE',  ( -0.000000000000000000, -1.000000000000000000, -0.000000000000000000 ) ) ;
#4982=ADVANCED_FACE ( 'NONE', ( #4010 ), #4844, .F. ) ;
#4985=CARTESIAN_POINT ( 'NONE',  ( -2.216580177477698310, 54.48481978330000430, 27.91250211204058473 ) ) ;
#5006=CARTESIAN_POINT ( 'NONE',  ( 3.548862490157215444, 10.64523530928737749, 24.74869899623665503 ) ) ;
#5016=CARTESIAN_POINT ( 'NONE',  ( 3.429011038972528284E-15, 30.00000000000001066, 28.00000000000000355 ) ) ;
#5019=CARTESIAN_POINT ( 'NONE',  ( 6.955575927950914131E-22, 45.00000000000000711, -25.00000000000000000 ) ) ;
#5028=CARTESIAN_POINT ( 'NONE',  ( 0.6563718250326410208, 10.01611854420673708, -27.99423098641389629 ) ) ;
#5045=EDGE_CURVE ( 'NONE', #2352, #10270, #8768, .T. ) ;
#5046=CARTESIAN_POINT ( 'NONE',  ( -3.767068525368503895, 53.30379312071067233, -24.71564595051174607 ) ) ;
#5051=CARTESIAN_POINT ( 'NONE',  ( 0.000000000000000000, 0.000000000000000000, -25.00000000000000000 ) ) ;
#5052=CARTESIAN_POINT ( 'NONE',  ( 9.660207172539163167, 22.60549549288601412, -26.28099775896728829 ) ) ;
#5057=ORIENTED_EDGE ( 'NONE', *, *, #4665, .F. ) ;
#5062=CARTESIAN_POINT ( 'NONE',  ( -8.664197377259947430, 14.96499702975700608, -23.45374477514955203 ) ) ;
#5065=CARTESIAN_POINT ( 'NONE',  ( -4.140053538423851224E-16, 30.00000000000001066, -28.00000000000000355 ) ) ;
#5071=CARTESIAN_POINT ( 'NONE',  ( -3.973686166794720975, 46.94757989445042767, 27.71721093970095495 ) ) ;
#5089=CARTESIAN_POINT ( 'NONE',  ( 4.832070635542911496, 51.29541901974291562, 27.57994638421516242 ) ) ;
#5091=CARTESIAN_POINT ( 'NONE',  ( 10.00000000000000355, 20.00000000000000355, -28.00000000000000711 ) ) ;
#5107=CARTESIAN_POINT ( 'NONE',  ( 0.6590680265247156333, 9.999999999999994671, 28.00000000000000355 ) ) ;
#5115=CARTESIAN_POINT ( 'NONE',  ( 2.286292697989654954, 29.74065845437095490, -27.90836410094387787 ) ) ;
#5127=CARTESIAN_POINT ( 'NONE',  ( 0.000000000000000000, 50.00000000000000000, -28.00000000000000711 ) ) ;
#5138=CARTESIAN_POINT ( 'NONE',  ( -10.00000000000000355, 19.67057089699415684, -26.15339366124403853 ) ) ;
#5139=EDGE_CURVE ( 'NONE', #4669, #6404, #578, .T. ) ;
#5160=CARTESIAN_POINT ( 'NONE',  ( -1.303021026755432743, 54.83843292061823149, -27.97152834316269576 ) ) ;
#5161=CARTESIAN_POINT ( 'NONE',  ( -4.831992280633556014, 48.70433893284562998, -27.57995989914503809 ) ) ;
#5168=CARTESIAN_POINT ( 'NONE',  ( -9.869611566543289527, 18.35654797443324782, 22.96945393929722457 ) ) ;
#5170=CARTESIAN_POINT ( 'NONE',  ( -9.659644484749870585, 22.60756928696590862, -26.28120473514388777 ) ) ;
#5175=AXIS2_PLACEMENT_3D ( 'NONE', #1126, #1062, #6945 ) ;
#5197=CARTESIAN_POINT ( 'NONE',  ( -0.6575419410981192536, 45.03270851040807088, 27.99410734628499853 ) ) ;
#5228=CARTESIAN_POINT ( 'NONE',  ( -8.488496443319393236, 14.70368316582932877, 23.51557330312556360 ) ) ;
#5230=CARTESIAN_POINT ( 'NONE',  ( -7.946804781952113927, 26.10495865974165142, 26.85128829824916252 ) ) ;
#5233=CARTESIAN_POINT ( 'NONE',  ( 8.671847030689137981, 14.97805994402878227, 26.62596067411855572 ) ) ;
#5234=CARTESIAN_POINT ( 'NONE',  ( 4.967195524026380760, 49.34122594216266577, -27.55596498020302576 ) ) ;
#5246=EDGE_LOOP ( 'NONE', ( #5973, #9831, #4348, #3181, #12140, #7642, #806, #11745, #3969, #8957, #6172, #2425, #3934, #5305, #12341, #10242 ) ) ;
#5247=CARTESIAN_POINT ( 'NONE',  ( -9.868061339005878452, 18.34793401400264301, -22.97011835729309936 ) ) ;
#5251=CARTESIAN_POINT ( 'NONE',  ( 4.741482771685880948, 51.61996731904482516, 24.54657867284130646 ) ) ;
#5262=CARTESIAN_POINT ( 'NONE',  ( -9.484541375895036097, 16.76356961828979308, -26.34605997290420376 ) ) ;
#5263=CARTESIAN_POINT ( 'NONE',  ( 7.931072658818332677, 13.90045964729634420, -26.85413380561048413 ) ) ;
#5288=ORIENTED_EDGE ( 'NONE', *, *, #8089, .F. ) ;
#5291=ORIENTED_EDGE ( 'NONE', *, *, #1344, .T. ) ;
#5297=EDGE_CURVE ( 'NONE', #7533, #6466, #9901, .T. ) ;
#5299=CARTESIAN_POINT ( 'NONE',  ( 3.245314017740486159E-15, 70.00000000000000000, 25.00000000000000000 ) ) ;
#5302=CARTESIAN_POINT ( 'NONE',  ( 10.00000000000000355, 20.00000000000000355, 26.15339366124404563 ) ) ;
#5305=ORIENTED_EDGE ( 'NONE', *, *, #3273, .F. ) ;
#5313=CARTESIAN_POINT ( 'NONE',  ( -8.972964902253410813, 15.53670184611763005, -23.33582545272828312 ) ) ;
#5324=CARTESIAN_POINT ( 'NONE',  ( -4.743460743378065558, 51.61424263853129446, 24.54619549801029166 ) ) ;
#5330=CARTESIAN_POINT ( 'NONE',  ( 8.486510062750307171, 14.70060591898896618, -23.51628241912814588 ) ) ;
#5348=ORIENTED_EDGE ( 'NONE', *, *, #9091, .F. ) ;
#5365=CARTESIAN_POINT ( 'NONE',  ( 0.6589055310361571216, 30.00000000000001776, 28.00000000000001421 ) ) ;
#5368=EDGE_CURVE ( 'NONE', #2615, #850, #7675, .T. ) ;
#5370=CARTESIAN_POINT ( 'NONE',  ( 4.840263798742708623, 51.29555919482307758, -24.52704763417973410 ) ) ;
#5372=ORIENTED_EDGE ( 'NONE', *, *, #3045, .T. ) ;
#5390=B_SPLINE_CURVE_WITH_KNOTS ( 'NONE', 3,
 ( #9298, #3209, #7071, #10948, #12088, #7257, #11132, #12275, #4654, #1733, #11381, #4593, #5737, #8404, #604, #12334, #4465, #8585, #2751, #2687 ),
 .UNSPECIFIED., .F., .F.,
 ( 4, 2, 2, 2, 2, 2, 2, 2, 2, 4 ),
 ( 0.007837842730401771429, 0.008817088216258357411, 0.009796333702114945127, 0.01028595644504323552, 0.01077557918797152590, 0.01175482467382810668, 0.01273407015968468919, 0.01371331564554126997, 0.01469256113139785075, 0.01567180661725443153 ),
 .UNSPECIFIED. ) ;
#5403=VECTOR ( 'NONE', #7727, 1000.000000000000000 ) ;
#5405=CARTESIAN_POINT ( 'NONE',  ( -4.743784540849714126, 51.61351337007339168, -27.59551847071385566 ) ) ;
#5410=EDGE_CURVE ( 'NONE', #2987, #3859, #9101, .T. ) ;
#5412=VERTEX_POINT ( 'NONE', #3915 ) ;
#5417=CARTESIAN_POINT ( 'NONE',  ( -9.935474497414313433, 21.31256710255370379, -26.17833964914451172 ) ) ;
#5460=CARTESIAN_POINT ( 'NONE',  ( 5.000000000000000000, 50.00000000000000000, 24.49489742783178059 ) ) ;
#5479=ORIENTED_EDGE ( 'NONE', *, *, #8808, .T. ) ;
#5482=ORIENTED_EDGE ( 'NONE', *, *, #471, .F. ) ;
#5483=CARTESIAN_POINT ( 'NONE',  ( -7.530077746149031803, 26.61198218432872764, -26.97262320105976485 ) ) ;
#5537=CARTESIAN_POINT ( 'NONE',  ( 8.664233696039474353, 25.03468766560890302, 23.45371044974007901 ) ) ;
#5542=ORIENTED_EDGE ( 'NONE', *, *, #3045, .F. ) ;
#5543=CARTESIAN_POINT ( 'NONE',  ( -3.709758735690515970E-18, 30.00000000000001066, -25.00000000000000000 ) ) ;
#5546=CARTESIAN_POINT ( 'NONE',  ( 2.294321452706637121, 29.73876067080973229, -24.89658462890612967 ) ) ;
#5571=AXIS2_PLACEMENT_3D ( 'NONE', #12425, #9514, #4815 ) ;
#5573=VERTEX_POINT ( 'NONE', #8172 ) ;
#5581=DIRECTION ( 'NONE',  ( 1.000000000000000000, 0.000000000000000000, 0.000000000000000000 ) ) ;
#5602=FACE_OUTER_BOUND ( 'NONE', #8839, .T. ) ;
#5623=CARTESIAN_POINT ( 'NONE',  ( -9.103371648737914157, 24.15160165414906857, 23.28405058525132176 ) ) ;
#5631=ORIENTED_EDGE ( 'NONE', *, *, #2384, .T. ) ;
#5634=EDGE_CURVE ( 'NONE', #6052, #6404, #11143, .T. ) ;
#5642=CARTESIAN_POINT ( 'NONE',  ( 3.304318396371782818, 46.23341735054634682, 27.80530896451984191 ) ) ;
#5643=CIRCLE ( 'NONE', #4622, 25.00000000000000355 ) ;
#5664=CARTESIAN_POINT ( 'NONE',  ( -6.102784694457409564, 27.94841462573825197, -27.33237746279936076 ) ) ;
#5670=CARTESIAN_POINT ( 'NONE',  ( 4.246185771498899975, 47.35493673757640920, -27.67631243003367558 ) ) ;
#5673=CARTESIAN_POINT ( 'NONE',  ( -1.299134361814098693, 45.16046244081530858, -27.97171976766272294 ) ) ;
#5678=DIRECTION ( 'NONE',  ( 1.000000000000000000, 0.000000000000000000, 0.000000000000000000 ) ) ;
#5681=CARTESIAN_POINT ( 'NONE',  ( 0.3310707342383826801, 55.00000000000000711, -24.99999999999999645 ) ) ;
#5687=FACE_OUTER_BOUND ( 'NONE', #607, .T. ) ;
#5688=CARTESIAN_POINT ( 'NONE',  ( -9.983825383151277322, 20.65789756057008120, 22.91995855732452370 ) ) ;
#5706=DIRECTION ( 'NONE',  ( -0.000000000000000000, -1.000000000000000000, -0.000000000000000000 ) ) ;
#5710=CARTESIAN_POINT ( 'NONE',  ( 3.061616998149962604E-15, 10.00000000000000000, 25.00000000000000000 ) ) ;
#5737=CARTESIAN_POINT ( 'NONE',  ( -3.974987698915826595, 46.94954269600466290, 24.68264807992340337 ) ) ;
#5743=CARTESIAN_POINT ( 'NONE',  ( -9.466558637120989772, 23.23925856829589520, -23.13860710034107626 ) ) ;
#5744=ADVANCED_FACE ( 'NONE', ( #9497 ), #4729, .T. ) ;
#5746=CARTESIAN_POINT ( 'NONE',  ( -6.109221465413982699, 27.94329460785578689, 24.24832107967536388 ) ) ;
#5752=CARTESIAN_POINT ( 'NONE',  ( 5.000000000000002665, 50.32693827311778278, -27.54995462791183058 ) ) ;
#5753=CARTESIAN_POINT ( 'NONE',  ( -5.299351711406078635, 11.51344256626987139, 27.49531132660919397 ) ) ;
#5763=DIRECTION ( 'NONE',  ( 0.000000000000000000, 0.000000000000000000, -1.000000000000000000 ) ) ;
#5775=( GEOMETRIC_REPRESENTATION_CONTEXT ( 3 ) GLOBAL_UNCERTAINTY_ASSIGNED_CONTEXT ( ( #7976 ) ) GLOBAL_UNIT_ASSIGNED_CONTEXT ( ( #11878, #8759, #76 ) ) REPRESENTATION_CONTEXT ( 'NONE', 'WORKASPACE' ) );
#5791=CARTESIAN_POINT ( 'NONE',  ( 8.666387210823231158, 14.96869202851870462, -26.62774317806001179 ) ) ;
#5809=CARTESIAN_POINT ( 'NONE',  ( 3.429011071898990822E-15, 55.00000000000000000, 28.00000000000000355 ) ) ;
#5813=CARTESIAN_POINT ( 'NONE',  ( 4.339334521168333403, 52.50564928449409052, -27.66232676752730768 ) ) ;
#5824=CARTESIAN_POINT ( 'NONE',  ( -10.00000000000000355, 20.00000000000000355, 26.15339366124404208 ) ) ;
#5869=CARTESIAN_POINT ( 'NONE',  ( -5.033342733373901368, 28.66546597776486038, -24.49435860509168350 ) ) ;
#5880=CARTESIAN_POINT ( 'NONE',  ( 0.000000000000000000, -4.262400816306111331E-15, 0.000000000000000000 ) ) ;
#5893=EDGE_CURVE ( 'NONE', #10229, #6052, #10870, .T. ) ;
#5916=CARTESIAN_POINT ( 'NONE',  ( 8.124733646131113929, 14.16101164777853150, -26.79597818126044473 ) ) ;
#5919=CARTESIAN_POINT ( 'NONE',  ( -3.294598684565033704E-22, 45.00000000000000711, -28.00000000000000355 ) ) ;
#5923=CARTESIAN_POINT ( 'NONE',  ( 0.000000000000000000, 20.00000000000000355, -28.00000000000000711 ) ) ;
#5930=CARTESIAN_POINT ( 'NONE',  ( -10.00000000000000533, 20.66054119461773553, -22.91287847477919470 ) ) ;
#5948=EDGE_CURVE ( 'NONE', #12211, #11194, #2689, .T. ) ;
#5958=CARTESIAN_POINT ( 'NONE',  ( -2.615680359617244211, 10.32552686981736123, -27.88513211093687971 ) ) ;
#5973=ORIENTED_EDGE ( 'NONE', *, *, #5297, .F. ) ;
#5974=LINE ( 'NONE', #5091, #6794 ) ;
#5992=CARTESIAN_POINT ( 'NONE',  ( 9.741406019701777552, 17.71702429258190747, 26.25089909648496089 ) ) ;
#5993=PRODUCT ( 'Bolt-Mounted Retaining Cylinder', 'Bolt-Mounted Retaining Cylinder', '', ( #1210 ) ) ;
#6001=CARTESIAN_POINT ( 'NONE',  ( 3.548616897151023686, 29.35492511944846683, -27.77589733847015552 ) ) ;
#6018=CARTESIAN_POINT ( 'NONE',  ( -4.743629175984715118, 48.38625991566029683, 27.59554290692945600 ) ) ;
#6028=CARTESIAN_POINT ( 'NONE',  ( 6.114177788104627531, 12.06044222946883693, -24.24708634001311580 ) ) ;
#6043=CARTESIAN_POINT ( 'NONE',  ( -4.338105965527106811, 47.49259679719147442, -27.66250853831607515 ) ) ;
#6051=CARTESIAN_POINT ( 'NONE',  ( -1.325835098444672733, 10.08270123135439711, 24.96701611100131402 ) ) ;
#6052=VERTEX_POINT ( 'NONE', #2985 ) ;
#6055=CARTESIAN_POINT ( 'NONE',  ( 6.614707539609227638, 12.47232065379156118, 27.21157843939673171 ) ) ;
#6062=CARTESIAN_POINT ( 'NONE',  ( -4.493707279255195530, 52.21668117324033176, 27.63734306083194880 ) ) ;
#6075=CARTESIAN_POINT ( 'NONE',  ( -9.917336477930691174, 18.67442475474294028, -22.94880690262607459 ) ) ;
#6085=CARTESIAN_POINT ( 'NONE',  ( -4.999999999999999112, 49.67329211228921082, 27.54995462791181993 ) ) ;
#6089=CARTESIAN_POINT ( 'NONE',  ( -7.935173117706110446, 13.90589240354496248, -26.85291110300881101 ) ) ;
#6098=ORIENTED_EDGE ( 'NONE', *, *, #10591, .T. ) ;
#6101=ORIENTED_EDGE ( 'NONE', *, *, #5410, .F. ) ;
#6108=CARTESIAN_POINT ( 'NONE',  ( -2.220456136781088219, 54.49171428740054068, -27.91344310064364009 ) ) ;
#6113=VERTEX_POINT ( 'NONE', #4952 ) ;
#6124=PRODUCT_DEFINITION_CONTEXT ( 'detailed design', #12179, 'design' ) ;
#6127=CARTESIAN_POINT ( 'NONE',  ( 3.429011037612589670E-15, 0.000000000000000000, 28.00000000000000355 ) ) ;
#6128=CARTESIAN_POINT ( 'NONE',  ( 2.290457103807213457, 29.73981914200485477, 24.89699738223682246 ) ) ;
#6130=EDGE_LOOP ( 'NONE', ( #389, #11583 ) ) ;
#6143=CARTESIAN_POINT ( 'NONE',  ( -1.765688943715743031, 45.31926316749526507, 27.94468539932264406 ) ) ;
#6147=CARTESIAN_POINT ( 'NONE',  ( -4.967147891453746134, 49.34082981697670078, -24.50166768924217564 ) ) ;
#6148=ORIENTED_EDGE ( 'NONE', *, *, #612, .T. ) ;
#6149=CARTESIAN_POINT ( 'NONE',  ( -0.6582364880112170358, 54.96720335004231828, 24.99338302292539638 ) ) ;
#6159=VERTEX_POINT ( 'NONE', #5016 ) ;
#6172=ORIENTED_EDGE ( 'NONE', *, *, #67, .F. ) ;
#6177=CARTESIAN_POINT ( 'NONE',  ( -9.483329012715213224, 23.23888378086489581, 26.34647234298155993 ) ) ;
#6179=CARTESIAN_POINT ( 'NONE',  ( 2.608216138242892335, 10.34052515137489969, 27.88005196315802792 ) ) ;
#6186=CARTESIAN_POINT ( 'NONE',  ( 5.018622449780372641, 28.67437547244667684, 27.55219550168085263 ) ) ;
#6194=CARTESIAN_POINT ( 'NONE',  ( -0.6576044892141179599, 10.01619439626406383, -24.99350884773162207 ) ) ;
#6206=CARTESIAN_POINT ( 'NONE',  ( 3.429010155815331973E-15, 45.00000000000000711, 28.00000000000000355 ) ) ;
#6208=CARTESIAN_POINT ( 'NONE',  ( -1.612729787338046394, 45.25594143338945941, -24.94976830077123964 ) ) ;
#6210=CARTESIAN_POINT ( 'NONE',  ( -4.556215257066872582, 52.06578128350423640, 24.58139409886873139 ) ) ;
#6220=EDGE_CURVE ( 'NONE', #1348, #8883, #7098, .T. ) ;
#6224=VERTEX_POINT ( 'NONE', #134 ) ;
#6230=CARTESIAN_POINT ( 'NONE',  ( -2.501722953165860464, 45.66777005292055236, -27.88839186769926215 ) ) ;
#6235=ORIENTED_EDGE ( 'NONE', *, *, #160, .F. ) ;
#6237=CARTESIAN_POINT ( 'NONE',  ( -10.00000000000001066, 19.67111324348436696, 22.91287847477920536 ) ) ;
#6256=CARTESIAN_POINT ( 'NONE',  ( -9.983516779091171855, 19.33659569722678029, -22.92009366892111899 ) ) ;
#6261=CARTESIAN_POINT ( 'NONE',  ( 3.298734236876446957, 53.76100060739371145, 24.78173945428942204 ) ) ;
#6269=VECTOR ( 'NONE', #10913, 1000.000000000000000 ) ;
#6272=ORIENTED_EDGE ( 'NONE', *, *, #2188, .F. ) ;
#6273=CARTESIAN_POINT ( 'NONE',  ( -7.304238131681169754, 13.16224956375578081, -27.03155692136176214 ) ) ;
#6279=CARTESIAN_POINT ( 'NONE',  ( 9.482520708152488709, 16.75818430496380529, -23.13341755400983502 ) ) ;
#6301=CARTESIAN_POINT ( 'NONE',  ( -5.845694806184612347, 11.88009017893230990, 24.30851799965319060 ) ) ;
#6304=CARTESIAN_POINT ( 'NONE',  ( -8.968509794689500936, 24.43547164034384878, 26.52531781923291376 ) ) ;
#6314=CARTESIAN_POINT ( 'NONE',  ( 7.928997479961922501, 26.10222245235190641, 26.85474570151987450 ) ) ;
#6327=CARTESIAN_POINT ( 'NONE',  ( -7.533400678184611898, 13.39129849816836249, 26.97176181097763958 ) ) ;
#6351=CARTESIAN_POINT ( 'NONE',  ( -4.840361584771153858, 51.29513118448893749, -27.57852565106875886 ) ) ;
#6356=CARTESIAN_POINT ( 'NONE',  ( 9.737811142203947057, 22.29842083447240597, 23.02563804066124931 ) ) ;
#6361=CARTESIAN_POINT ( 'NONE',  ( -10.00000000000000355, 20.00000000000000355, 22.91287847477919826 ) ) ;
#6362=ORIENTED_EDGE ( 'NONE', *, *, #9800, .F. ) ;
#6374=CARTESIAN_POINT ( 'NONE',  ( 6.610911640192685290, 27.53087490925221559, 27.21248546868482876 ) ) ;
#6399=CARTESIAN_POINT ( 'NONE',  ( 9.105349949761121664, 15.85277269881838258, -23.28327519851026040 ) ) ;
#6404=VERTEX_POINT ( 'NONE', #12426 ) ;
#6415=CARTESIAN_POINT ( 'NONE',  ( 5.303296350723960551, 28.48414319546200346, 24.43259468344301055 ) ) ;
#6427=CARTESIAN_POINT ( 'NONE',  ( 4.330144968755956114, 47.49467013450670549, -27.66326046019273832 ) ) ;
#6432=CARTESIAN_POINT ( 'NONE',  ( -3.294598684565033704E-22, 45.00000000000000711, -28.00000000000000355 ) ) ;
#6436=VERTEX_POINT ( 'NONE', #12366 ) ;
#6437=CARTESIAN_POINT ( 'NONE',  ( 7.192769615190809278E-19, 10.00000000000000000, -28.00000000000000355 ) ) ;
#6438=ORIENTED_EDGE ( 'NONE', *, *, #160, .T. ) ;
#6466=VERTEX_POINT ( 'NONE', #2779 ) ;
#6478=ORIENTED_EDGE ( 'NONE', *, *, #12427, .T. ) ;
#6484=CARTESIAN_POINT ( 'NONE',  ( 8.654532730718658584, 25.02058024782134282, -23.45477484801500623 ) ) ;
#6486=CARTESIAN_POINT ( 'NONE',  ( 10.00000000000000355, 20.00000000000000355, -26.15339366124404208 ) ) ;
#6493=CARTESIAN_POINT ( 'NONE',  ( 0.000000000000000000, 20.00000000000000355, -28.00000000000000711 ) ) ;
#6499=ORIENTED_EDGE ( 'NONE', *, *, #3662, .T. ) ;
#6534=CARTESIAN_POINT ( 'NONE',  ( 7.931687869515056555, 26.09867752937626406, 23.70939416258605803 ) ) ;
#6557=VERTEX_POINT ( 'NONE', #4876 ) ;
#6565=CARTESIAN_POINT ( 'NONE',  ( -9.673352204464322313, 22.61971715202064104, 23.05311956053869338 ) ) ;
#6575=VERTEX_POINT ( 'NONE', #3031 ) ;
#6599=CARTESIAN_POINT ( 'NONE',  ( -2.601079580437228422, 29.66139515859289233, -27.88071816736361441 ) ) ;
#6604=CARTESIAN_POINT ( 'NONE',  ( 2.509417286374489020, 45.66310105023414678, -27.88864816121832746 ) ) ;
#6615=CARTESIAN_POINT ( 'NONE',  ( 2.508429781980343609, 54.33777489521010295, -24.87536199211671573 ) ) ;
#6616=ORIENTED_EDGE ( 'NONE', *, *, #6220, .F. ) ;
#6619=CARTESIAN_POINT ( 'NONE',  ( -6.610481451048220158, 27.51047402958706201, -24.11159121895188306 ) ) ;
#6621=DIRECTION ( 'NONE',  ( 1.000000000000000000, 0.000000000000000000, 0.000000000000000000 ) ) ;
#6625=ORIENTED_EDGE ( 'NONE', *, *, #2085, .T. ) ;
#6626=CARTESIAN_POINT ( 'NONE',  ( 5.000000000000000000, 50.00000000000000000, -27.54995462791182703 ) ) ;
#6627=CYLINDRICAL_SURFACE ( 'NONE', #8989, 5.000000000000000000 ) ;
#6633=VERTEX_POINT ( 'NONE', #8935 ) ;
#6644=CARTESIAN_POINT ( 'NONE',  ( 0.6608155348566246978, 10.00000000000000178, 24.99999999999999645 ) ) ;
#6648=AXIS2_PLACEMENT_3D ( 'NONE', #5923, #10601, #11632 ) ;
#6679=CARTESIAN_POINT ( 'NONE',  ( 1.620000493755592075, 54.74147302055352071, -24.94927790585931504 ) ) ;
#6686=DIRECTION ( 'NONE',  ( -0.000000000000000000, -1.000000000000000000, -0.000000000000000000 ) ) ;
#6687=CARTESIAN_POINT ( 'NONE',  ( -7.300087775502666965, 26.84214942138161675, 23.91163959704068631 ) ) ;
#6693=CARTESIAN_POINT ( 'NONE',  ( 2.220191578079284245, 54.49201116149205149, -27.91348774472430705 ) ) ;
#6694=CARTESIAN_POINT ( 'NONE',  ( -5.021298913057436586, 11.34591840113689365, 27.54762567907054205 ) ) ;
#6725=VERTEX_POINT ( 'NONE', #3287 ) ;
#6728=CARTESIAN_POINT ( 'NONE',  ( 1.642686742655169674, 10.13030119466746015, -27.95366245041864417 ) ) ;
#6751=CARTESIAN_POINT ( 'NONE',  ( 5.028136979683376140, 28.66851506631811120, -27.55037744543317757 ) ) ;
#6756=FACE_OUTER_BOUND ( 'NONE', #9863, .T. ) ;
#6769=CARTESIAN_POINT ( 'NONE',  ( 1.614286760591197245, 45.25655306502918762, -24.94965407877490549 ) ) ;
#6770=CONICAL_SURFACE ( 'NONE', #1513, 28.00000000000000000, 0.7853981633974477239 ) ;
#6774=CARTESIAN_POINT ( 'NONE',  ( 9.353363810095283171, 16.44731154698707698, 23.18475774758237407 ) ) ;
#6794=VECTOR ( 'NONE', #6985, 1000.000000000000000 ) ;
#6795=CARTESIAN_POINT ( 'NONE',  ( 7.192769615190809278E-19, 10.00000000000000000, -28.00000000000000355 ) ) ;
#6811=CARTESIAN_POINT ( 'NONE',  ( -3.709758735690515970E-18, 30.00000000000001066, -25.00000000000000000 ) ) ;
#6812=CARTESIAN_POINT ( 'NONE',  ( -2.220795175011430533, 54.49171124227147089, -24.90301599942658228 ) ) ;
#6827=EDGE_CURVE ( 'NONE', #10270, #6633, #8825, .T. ) ;
#6860=CARTESIAN_POINT ( 'NONE',  ( 1.312601162367561303, 10.08103881020897319, -27.97114353547140908 ) ) ;
#6874=CARTESIAN_POINT ( 'NONE',  ( -9.740943735563897476, 22.28537929251632477, -23.02431258361445288 ) ) ;
#6880=CARTESIAN_POINT ( 'NONE',  ( 2.604960375799227901, 29.66039127547307785, -27.88036871804450101 ) ) ;
#6890=DIRECTION ( 'NONE',  ( -0.000000000000000000, -0.000000000000000000, 1.000000000000000000 ) ) ;
#6897=LINE ( 'NONE', #7921, #11668 ) ;
#6900=ORIENTED_EDGE ( 'NONE', *, *, #7131, .T. ) ;
#6902=SHAPE_DEFINITION_REPRESENTATION ( #2136, #4339 ) ;
#6907=CARTESIAN_POINT ( 'NONE',  ( 5.307486386703490489, 11.51851869311760090, -24.43167369944409018 ) ) ;
#6912=ADVANCED_FACE ( 'NONE', ( #6756 ), #6627, .F. ) ;
#6913=FACE_OUTER_BOUND ( 'NONE', #5246, .T. ) ;
#6933=CARTESIAN_POINT ( 'NONE',  ( 9.469886687176911622, 16.77055699046783843, 26.35017345530262745 ) ) ;
#6939=CARTESIAN_POINT ( 'NONE',  ( -3.975160125666882482, 53.05023972334481641, 27.71699044896146447 ) ) ;
#6945=DIRECTION ( 'NONE',  ( 0.000000000000000000, 0.000000000000000000, -1.000000000000000000 ) ) ;
#6951=CARTESIAN_POINT ( 'NONE',  ( -3.245616027290198602, 10.51897860477085622, -24.79588311023535852 ) ) ;
#6953=CARTESIAN_POINT ( 'NONE',  ( 0.000000000000000000, -4.262400816306111331E-15, -28.00000000000000355 ) ) ;
#6954=CARTESIAN_POINT ( 'NONE',  ( 3.061565168526138680E-15, 55.00000000000000000, 25.00000000000000000 ) ) ;
#6956=CARTESIAN_POINT ( 'NONE',  ( 4.967203680380478659, 49.34177296812513447, -24.50165547367289065 ) ) ;
#6970=CARTESIAN_POINT ( 'NONE',  ( 0.000000000000000000, 20.00000000000000355, -28.00000000000000711 ) ) ;
#6977=ORIENTED_EDGE ( 'NONE', *, *, #1010, .T. ) ;
#6978=CARTESIAN_POINT ( 'NONE',  ( 0.000000000000000000, 0.000000000000000000, 0.000000000000000000 ) ) ;
#6981=VECTOR ( 'NONE', #4097, 1000.000000000000114 ) ;
#6984=ORIENTED_EDGE ( 'NONE', *, *, #7346, .T. ) ;
#6985=DIRECTION ( 'NONE',  ( -0.000000000000000000, -0.000000000000000000, 1.000000000000000000 ) ) ;
#6990=CARTESIAN_POINT ( 'NONE',  ( -5.000000000000000000, 49.66965428365661239, -27.54995462791182348 ) ) ;
#7011=CARTESIAN_POINT ( 'NONE',  ( 10.00000000000000000, 20.65873750777989670, -26.15339366124403497 ) ) ;
#7018=LINE ( 'NONE', #8924, #6981 ) ;
#7019=CARTESIAN_POINT ( 'NONE',  ( -10.00000000000000355, 20.00000000000000355, -22.91287847477919826 ) ) ;
#7023=CARTESIAN_POINT ( 'NONE',  ( 2.502435999373153308, 45.66817884423451801, -24.87486459250430926 ) ) ;
#7029=ORIENTED_EDGE ( 'NONE', *, *, #235, .T. ) ;
#7038=CARTESIAN_POINT ( 'NONE',  ( -5.000000000000000000, 50.00000000000000000, -28.00000000000000711 ) ) ;
#7042=ORIENTED_EDGE ( 'NONE', *, *, #11233, .T. ) ;
#7054=ORIENTED_EDGE ( 'NONE', *, *, #471, .T. ) ;
#7071=CARTESIAN_POINT ( 'NONE',  ( -0.6591801397249409389, 45.03285316749953182, 24.99337097521990003 ) ) ;
#7079=CARTESIAN_POINT ( 'NONE',  ( -9.481501190889247255, 16.75403870714897536, -23.13387092261990574 ) ) ;
#7089=CARTESIAN_POINT ( 'NONE',  ( -4.838879514055022923, 48.69911239754581089, -24.52732196506755713 ) ) ;
#7091=CARTESIAN_POINT ( 'NONE',  ( -3.973554925899839052, 53.05255087154787219, 24.68288788663009825 ) ) ;
#7096=CARTESIAN_POINT ( 'NONE',  ( 0.6581862696184550554, 10.01618719080246578, -24.99351150626209161 ) ) ;
#7098=LINE ( 'NONE', #7038, #6269 ) ;
#7115=CARTESIAN_POINT ( 'NONE',  ( -3.303799404834185438, 46.23288169458685104, -27.80537610472761045 ) ) ;
#7123=EDGE_LOOP ( 'NONE', ( #6438, #12062, #3001, #7579 ) ) ;
#7131=EDGE_CURVE ( 'NONE', #2352, #12211, #9131, .T. ) ;
#7132=CARTESIAN_POINT ( 'NONE',  ( 9.933961117401199914, 21.32149700181756558, 26.17890995529624476 ) ) ;
#7139=CARTESIAN_POINT ( 'NONE',  ( -10.00000000000000355, 19.66998333124466214, -22.91287847477919826 ) ) ;
#7142=LINE ( 'NONE', #11019, #10071 ) ;
#7143=LINE ( 'NONE', #493, #1564 ) ;
#7149=CARTESIAN_POINT ( 'NONE',  ( -4.556456226338131188, 47.93475174319672760, 27.62684759756936970 ) ) ;
#7151=LINE ( 'NONE', #8113, #7505 ) ;
#7168=B_SPLINE_CURVE_WITH_KNOTS ( 'NONE', 3,
 ( #9802, #5107, #352, #4216, #6179, #1366, #2183, #9104, #4018, #11763, #4149, #8088, #6055, #11895, #3199, #5233, #1112, #11064, #6933, #2116, #5992, #10349, #1665, #717 ),
 .UNSPECIFIED., .F., .F.,
 ( 4, 2, 2, 2, 2, 2, 2, 2, 2, 2, 2, 4 ),
 ( 0.04728207046791076812, 0.04925237334111622067, 0.05023752477771894348, 0.05122267621432167323, 0.05220782765092439603, 0.05319297908752712578, 0.05516328196073257140, 0.05713358483393803089, 0.05910388770714347650, 0.06008903914374620625, 0.06107419058034893600, 0.06304449345355438161 ),
 .UNSPECIFIED. ) ;
#7172=VECTOR ( 'NONE', #10881, 1000.000000000000000 ) ;
#7180=VECTOR ( 'NONE', #8336, 1000.000000000000000 ) ;
#7184=CARTESIAN_POINT ( 'NONE',  ( -9.918969497010245107, 21.31253892522589055, 26.18425576506515640 ) ) ;
#7187=CARTESIAN_POINT ( 'NONE',  ( 4.555810879675650682, 47.93324276400543482, -27.62695503246266071 ) ) ;
#7194=LINE ( 'NONE', #9237, #1983 ) ;
#7214=CARTESIAN_POINT ( 'NONE',  ( -0.3266958997752330562, 45.00000000000001421, -25.00000000000000355 ) ) ;
#7256=LINE ( 'NONE', #6127, #292 ) ;
#7257=CARTESIAN_POINT ( 'NONE',  ( -2.067585255946370548, 45.44456205236168245, 24.91481882275639848 ) ) ;
#7270=AXIS2_PLACEMENT_3D ( 'NONE', #2445, #1563, #9306 ) ;
#7271=CARTESIAN_POINT ( 'NONE',  ( 5.000000000000000000, 50.00000000000000000, 24.49489742783178059 ) ) ;
#7306=ORIENTED_EDGE ( 'NONE', *, *, #7346, .F. ) ;
#7310=CARTESIAN_POINT ( 'NONE',  ( -0.3292543530451116363, 30.00000000000001421, 28.00000000000000355 ) ) ;
#7324=CARTESIAN_POINT ( 'NONE',  ( 3.968701803879573831, 53.04568146648268367, -24.68320166897649770 ) ) ;
#7346=EDGE_CURVE ( 'NONE', #3859, #6557, #8841, .T. ) ;
#7361=CARTESIAN_POINT ( 'NONE',  ( -2.508609049021579551, 54.33766627009165262, -27.88875238525115208 ) ) ;
#7387=CARTESIAN_POINT ( 'NONE',  ( 3.761098173404043621, 53.29862245996868353, -24.71568690466639140 ) ) ;
#7390=ORIENTED_EDGE ( 'NONE', *, *, #3016, .T. ) ;
#7414=CARTESIAN_POINT ( 'NONE',  ( 2.505975641493357831, 45.66085398937747186, 24.87560495202607669 ) ) ;
#7419=CARTESIAN_POINT ( 'NONE',  ( 9.739739614376460963, 17.70973893131317922, 23.02482158226496622 ) ) ;
#7441=CARTESIAN_POINT ( 'NONE',  ( 3.302118497427160904, 46.23115272073012960, -27.80559317508241790 ) ) ;
#7451=CARTESIAN_POINT ( 'NONE',  ( 3.055841136373902422, 53.97118948954670969, -24.81406232681816348 ) ) ;
#7462=CARTESIAN_POINT ( 'NONE',  ( 1.766167014948355707, 54.68054567383913422, -27.94465362560199040 ) ) ;
#7468=EDGE_LOOP ( 'NONE', ( #1479, #7390, #11601, #9814 ) ) ;
#7481=CARTESIAN_POINT ( 'NONE',  ( 9.933637772289912959, 18.67556250305220189, 22.94215742280771408 ) ) ;
#7492=CARTESIAN_POINT ( 'NONE',  ( 2.612127725832936065, 29.65839247515747346, 24.86517017815632968 ) ) ;
#7500=CARTESIAN_POINT ( 'NONE',  ( -5.024113554834485740, 28.67061468857206563, -27.55106389568239322 ) ) ;
#7502=CARTESIAN_POINT ( 'NONE',  ( 7.942143053965557975, 26.11098614794844863, -23.70800582113895061 ) ) ;
#7505=VECTOR ( 'NONE', #10080, 1000.000000000000000 ) ;
#7509=B_SPLINE_CURVE_WITH_KNOTS ( 'NONE', 3,
 ( #12245, #3546, #7481, #7419, #11354, #10640, #6774, #1018, #1142, #7860, #7735, #9703, #3858, #1824, #10702, #11600, #10514, #5006, #11789, #8743, #948, #9641, #6644, #5710 ),
 .UNSPECIFIED., .F., .F.,
 ( 4, 2, 2, 2, 2, 2, 2, 2, 2, 2, 2, 4 ),
 ( 0.000000000000000000, 0.001975470015275241145, 0.002963205022912861284, 0.003950940030550481423, 0.005926410045825732976, 0.006914145053463355284, 0.007901880061100976724, 0.009877350076376223073, 0.01185282009165146769, 0.01284055509928909086, 0.01382829010692671404, 0.01580376012220196039 ),
 .UNSPECIFIED. ) ;
#7511=FACE_OUTER_BOUND ( 'NONE', #12060, .T. ) ;
#7512=ORIENTED_EDGE ( 'NONE', *, *, #8600, .F. ) ;
#7514=CARTESIAN_POINT ( 'NONE',  ( 3.307338549894080604, 53.76391169785250668, -24.78134996739077422 ) ) ;
#7527=CARTESIAN_POINT ( 'NONE',  ( 4.743569837746959728, 51.61387508005228142, -27.59555274614490017 ) ) ;
#7533=VERTEX_POINT ( 'NONE', #5299 ) ;
#7536=PLANE ( 'NONE',  #3987 ) ;
#7539=DIRECTION ( 'NONE',  ( 0.000000000000000000, 0.000000000000000000, -1.000000000000000000 ) ) ;
#7540=CARTESIAN_POINT ( 'NONE',  ( 0.3271393060908659445, 45.00000000000000711, 25.00000000000000355 ) ) ;
#7541=ADVANCED_FACE ( 'NONE', ( #8091 ), #2707, .T. ) ;
#7542=CARTESIAN_POINT ( 'NONE',  ( 0.000000000000000000, 67.00000000000000000, 0.000000000000000000 ) ) ;
#7562=APPLICATION_CONTEXT ( 'automotive_design' ) ;
#7566=CARTESIAN_POINT ( 'NONE',  ( 1.326742001580319741, 29.91711497655587948, -24.96694321103489855 ) ) ;
#7579=ORIENTED_EDGE ( 'NONE', *, *, #10397, .F. ) ;
#7587=CARTESIAN_POINT ( 'NONE',  ( -9.481431770954213079, 23.24517152888003224, 23.13387126485941536 ) ) ;
#7597=ORIENTED_EDGE ( 'NONE', *, *, #4345, .T. ) ;
#7604=LINE ( 'NONE', #7730, #4163 ) ;
#7606=CYLINDRICAL_SURFACE ( 'NONE', #5571, 10.00000000000000355 ) ;
#7632=CARTESIAN_POINT ( 'NONE',  ( 3.050317456283809570, 46.02489861342813526, -27.83468043274920234 ) ) ;
#7642=ORIENTED_EDGE ( 'NONE', *, *, #7131, .F. ) ;
#7651=CARTESIAN_POINT ( 'NONE',  ( -8.665812433443574132E-16, 55.00000000000000000, -28.00000000000000355 ) ) ;
#7656=EDGE_CURVE ( 'NONE', #7533, #2987, #3818, .T. ) ;
#7672=CARTESIAN_POINT ( 'NONE',  ( -3.241172199251822317, 10.51724913471846889, -27.81845307868313100 ) ) ;
#7675=B_SPLINE_CURVE_WITH_KNOTS ( 'NONE', 3,
 ( #2777, #12483, #2841, #11596, #6769, #8047, #11915, #7023, #1201, #7792, #3158, #9698, #10897, #7981, #11664, #3089, #1947, #6956, #3222, #247 ),
 .UNSPECIFIED., .F., .F.,
 ( 4, 2, 2, 2, 2, 2, 2, 2, 2, 4 ),
 ( 0.01567185795944686308, 0.01665140573566027682, 0.01763095351187368709, 0.01812072739998039222, 0.01861050128808709736, 0.01959004906430051110, 0.02056959684051392484, 0.02154914461672733511, 0.02252869239294074538, 0.02350824016915415912 ),
 .UNSPECIFIED. ) ;
#7708=CARTESIAN_POINT ( 'NONE',  ( -6.108719317430274742, 27.92396576624410187, -24.24357326025485193 ) ) ;
#7710=CARTESIAN_POINT ( 'NONE',  ( -1.322864546895947679, 29.91770977471893289, 24.96717945133217498 ) ) ;
#7717=CARTESIAN_POINT ( 'NONE',  ( 0.000000000000000000, -4.262400816306111331E-15, 0.000000000000000000 ) ) ;
#7727=DIRECTION ( 'NONE',  ( -0.000000000000000000, -1.000000000000000000, -0.000000000000000000 ) ) ;
#7729=DIRECTION ( 'NONE',  ( -0.000000000000000000, -1.000000000000000000, -0.000000000000000000 ) ) ;
#7730=CARTESIAN_POINT ( 'NONE',  ( 0.000000000000000000, 0.000000000000000000, -25.00000000000000000 ) ) ;
#7735=CARTESIAN_POINT ( 'NONE',  ( 7.927224944456558120, 13.89552811154835510, 23.71088769051724654 ) ) ;
#7749=CARTESIAN_POINT ( 'NONE',  ( 0.6519265100557631865, 54.96824252967201119, 27.99427508789008812 ) ) ;
#7765=ORIENTED_EDGE ( 'NONE', *, *, #5297, .T. ) ;
#7775=B_SPLINE_CURVE_WITH_KNOTS ( 'NONE', 3,
 ( #6486, #10083, #1907, #4962, #10857, #4066, #7945, #2868, #5791, #5916, #5263, #2931, #7879, #8824, #144, #8892, #11749, #8761, #9134, #2993, #3816, #6728, #6860, #5028, #10723, #6795 ),
 .UNSPECIFIED., .F., .F.,
 ( 4, 2, 2, 2, 2, 2, 2, 2, 2, 2, 2, 2, 4 ),
 ( 0.01576884472483168140, 0.01675373746250873042, 0.01773863020018578290, 0.01970841567553989482, 0.02167820115089400673, 0.02266309388857106616, 0.02364798662624812906, 0.02561777210160225138, 0.02660266483927931427, 0.02758755757695637717, 0.02955734305231050643, 0.03054223578998756933, 0.03152712852766463569 ),
 .UNSPECIFIED. ) ;
#7777=CARTESIAN_POINT ( 'NONE',  ( 10.00000000000000355, 20.00000000000000355, -26.15339366124404208 ) ) ;
#7785=CARTESIAN_POINT ( 'NONE',  ( -5.000000000000000000, 50.00000000000000000, 27.54995462791182348 ) ) ;
#7789=CARTESIAN_POINT ( 'NONE',  ( 3.061616997868383043E-15, 0.000000000000000000, 25.00000000000000000 ) ) ;
#7792=CARTESIAN_POINT ( 'NONE',  ( 3.052678183968668524, 46.02654057254596154, -24.81443426854575307 ) ) ;
#7795=CARTESIAN_POINT ( 'NONE',  ( 2.504536724946392567, 45.66016527775391154, 27.88910086977369573 ) ) ;
#7812=CARTESIAN_POINT ( 'NONE',  ( 3.764387367674736140, 53.30686585430343172, 27.74677055206694121 ) ) ;
#7825=CARTESIAN_POINT ( 'NONE',  ( 0.000000000000000000, 0.000000000000000000, 0.000000000000000000 ) ) ;
#7829=CARTESIAN_POINT ( 'NONE',  ( -5.038456156925416707, 11.33776630238819116, 24.49323865847078707 ) ) ;
#7842=ORIENTED_EDGE ( 'NONE', *, *, #10377, .T. ) ;
#7860=CARTESIAN_POINT ( 'NONE',  ( 8.123360751522579193, 14.15902104166613107, 23.64419573351483450 ) ) ;
#7863=CARTESIAN_POINT ( 'NONE',  ( -1.312971999154120883, 10.08108238931077238, -27.97112805829059212 ) ) ;
#7877=ORIENTED_EDGE ( 'NONE', *, *, #1010, .F. ) ;
#7879=CARTESIAN_POINT ( 'NONE',  ( 7.296171710155400447, 13.15373968915042546, -27.03372408122936221 ) ) ;
#7899=CARTESIAN_POINT ( 'NONE',  ( -3.768914454385754897, 53.30204245436056709, 27.74617514008307850 ) ) ;
#7912=CARTESIAN_POINT ( 'NONE',  ( -5.300214471940789096, 11.51392236371535382, -24.43326627631521220 ) ) ;
#7914=DIRECTION ( 'NONE',  ( 1.000000000000000000, 0.000000000000000000, 0.000000000000000000 ) ) ;
#7921=CARTESIAN_POINT ( 'NONE',  ( 5.000000000000000000, 50.00000000000000000, -28.00000000000000711 ) ) ;
#7929=DIRECTION ( 'NONE',  ( -0.000000000000000000, -0.000000000000000000, 1.000000000000000000 ) ) ;
#7933=CARTESIAN_POINT ( 'NONE',  ( 6.615773601782837687, 12.47291401044366310, -24.11353245396511014 ) ) ;
#7945=CARTESIAN_POINT ( 'NONE',  ( 9.483635936780883569, 16.76033569708264892, -26.34640174718215277 ) ) ;
#7948=CARTESIAN_POINT ( 'NONE',  ( -4.736720175570490632, 48.39053767382229410, -27.59648201160602454 ) ) ;
#7964=CARTESIAN_POINT ( 'NONE',  ( -3.050683747432114679, 53.97481441654883838, 27.83463951904226974 ) ) ;
#7976=UNCERTAINTY_MEASURE_WITH_UNIT (LENGTH_MEASURE( 1.000000000000000082E-05 ), #11878, 'distance_accuracy_value', 'NONE');
#7979=CARTESIAN_POINT ( 'NONE',  ( 2.912936886510098855, 54.06713064528141643, 24.83009325023465763 ) ) ;
#7981=CARTESIAN_POINT ( 'NONE',  ( 4.337692624494786209, 47.49191884430658206, -24.62149689268095187 ) ) ;
#7986=AXIS2_PLACEMENT_3D ( 'NONE', #7825, #9669, #10090 ) ;
#7989=CARTESIAN_POINT ( 'NONE',  ( -3.050580840359966128, 46.02510565206127779, -24.81467268664276560 ) ) ;
#7991=CARTESIAN_POINT ( 'NONE',  ( -6.111033161645041289, 12.05791699719159915, -27.33052924945952356 ) ) ;
#8005=CARTESIAN_POINT ( 'NONE',  ( 1.613904720388662728, 54.74356075780413988, 27.95507540029298710 ) ) ;
#8010=CARTESIAN_POINT ( 'NONE',  ( -3.052500473972970418, 46.02637407260866809, -27.83446103405789884 ) ) ;
#8025=CARTESIAN_POINT ( 'NONE',  ( -3.050747483057216769, 53.97487283205587261, -24.81466456749452831 ) ) ;
#8030=CARTESIAN_POINT ( 'NONE',  ( -5.000000000000000000, 50.00000000000000000, 27.54995462791182348 ) ) ;
#8047=CARTESIAN_POINT ( 'NONE',  ( 2.065847364689658683, 45.44381439048179772, -24.91495664786098274 ) ) ;
#8051=CARTESIAN_POINT ( 'NONE',  ( -3.306326722491793824, 46.23509958683961685, 27.80507441932701340 ) ) ;
#8054=CARTESIAN_POINT ( 'NONE',  ( -5.000000000000000888, 49.67303160952345564, -24.49489742783178059 ) ) ;
#8057=CARTESIAN_POINT ( 'NONE',  ( -1.297965663867492347, 54.83959394270241461, 24.96833505342767978 ) ) ;
#8065=ORIENTED_EDGE ( 'NONE', *, *, #10383, .F. ) ;
#8086=CARTESIAN_POINT ( 'NONE',  ( -6.102022788481106907, 27.92916547445571140, 27.32823034940942364 ) ) ;
#8088=CARTESIAN_POINT ( 'NONE',  ( 6.115126465005007006, 12.06069949568701283, 27.32969027731172673 ) ) ;
#8089=EDGE_CURVE ( 'NONE', #1348, #6557, #2619, .T. ) ;
#8091=FACE_OUTER_BOUND ( 'NONE', #7468, .T. ) ;
#8113=CARTESIAN_POINT ( 'NONE',  ( 5.000000000000000000, 50.00000000000000000, -28.00000000000000711 ) ) ;
#8151=CARTESIAN_POINT ( 'NONE',  ( 4.744280297632045951, 48.38773530922238564, -27.59543500301886354 ) ) ;
#8161=( NAMED_UNIT ( * ) SI_UNIT ( $, .STERADIAN. ) SOLID_ANGLE_UNIT ( ) );
#8166=CARTESIAN_POINT ( 'NONE',  ( -2.620496854523448604, 10.32661740714168097, -24.87086379260451707 ) ) ;
#8172=CARTESIAN_POINT ( 'NONE',  ( 5.000000000000000000, 50.00000000000000000, 27.54995462791182703 ) ) ;
#8173=FACE_OUTER_BOUND ( 'NONE', #8712, .T. ) ;
#8174=CARTESIAN_POINT ( 'NONE',  ( -9.918964982526143004, 18.68741511430571833, 26.18425748175654988 ) ) ;
#8175=DIRECTION ( 'NONE',  ( -0.000000000000000000, -0.000000000000000000, 1.000000000000000000 ) ) ;
#8179=CARTESIAN_POINT ( 'NONE',  ( -8.127975879305816775, 14.16556116651870845, -26.79499133733385108 ) ) ;
#8185=CARTESIAN_POINT ( 'NONE',  ( 9.917674697986294419, 18.67684296126092747, -22.94866065126248600 ) ) ;
#8207=CARTESIAN_POINT ( 'NONE',  ( -8.658175568303594360, 14.98574592473889311, 23.45342671841680371 ) ) ;
#8211=CARTESIAN_POINT ( 'NONE',  ( 3.061616997868383043E-15, 0.000000000000000000, 25.00000000000000000 ) ) ;
#8231=CARTESIAN_POINT ( 'NONE',  ( 3.419345135684301873, 53.65163791593241172, 24.76532955609361863 ) ) ;
#8240=CARTESIAN_POINT ( 'NONE',  ( -3.974640651900942512, 46.94910328357455143, -24.68270373814292640 ) ) ;
#8248=CARTESIAN_POINT ( 'NONE',  ( 9.673501139021151829, 17.38172013086462542, -23.05305332146628317 ) ) ;
#8275=ADVANCED_FACE ( 'NONE', ( #11794 ), #194, .F. ) ;
#8276=CARTESIAN_POINT ( 'NONE',  ( 0.000000000000000000, -3.000000000000003109, 0.000000000000000000 ) ) ;
#8279=CARTESIAN_POINT ( 'NONE',  ( 7.515035695928145465, 26.60532803001909841, 26.97351675661644421 ) ) ;
#8284=CARTESIAN_POINT ( 'NONE',  ( 4.067198847596982247, 52.91284127144104588, -24.66711128229975003 ) ) ;
#8318=CARTESIAN_POINT ( 'NONE',  ( 0.000000000000000000, 67.00000000000000000, 0.000000000000000000 ) ) ;
#8328=CARTESIAN_POINT ( 'NONE',  ( 10.00000000000000355, 20.00000000000000355, 22.91287847477919826 ) ) ;
#8330=ORIENTED_EDGE ( 'NONE', *, *, #4417, .T. ) ;
#8334=CARTESIAN_POINT ( 'NONE',  ( -8.489225034269651360, 25.29515013360644460, 26.68274546775624145 ) ) ;
#8336=DIRECTION ( 'NONE',  ( -0.000000000000000000, -1.000000000000000000, -0.000000000000000000 ) ) ;
#8343=CARTESIAN_POINT ( 'NONE',  ( 7.297108714790656592, 26.84519990999798367, 27.03346230006399509 ) ) ;
#8370=VECTOR ( 'NONE', #9077, 1000.000000000000000 ) ;
#8385=CARTESIAN_POINT ( 'NONE',  ( 0.6586899486374204749, 30.00000000000001421, 25.00000000000000000 ) ) ;
#8395=CARTESIAN_POINT ( 'NONE',  ( 3.549343885166972523, 29.35473140773891032, -24.74867856782190856 ) ) ;
#8399=EDGE_CURVE ( 'NONE', #6633, #10006, #3296, .T. ) ;
#8404=CARTESIAN_POINT ( 'NONE',  ( -4.336726535208759614, 47.49029485220934532, 24.62166619875052831 ) ) ;
#8419=CARTESIAN_POINT ( 'NONE',  ( -5.837112373185870062, 11.87393669850012756, 27.38618981624034632 ) ) ;
#8458=CARTESIAN_POINT ( 'NONE',  ( 1.612114502486744261, 45.25572168872454881, -27.95519462443614955 ) ) ;
#8467=CARTESIAN_POINT ( 'NONE',  ( 2.221110608488543026, 54.49139573732541209, -24.90296241992962578 ) ) ;
#8474=CARTESIAN_POINT ( 'NONE',  ( -10.00000000000000355, 20.00000000000000355, 22.91287847477919826 ) ) ;
#8480=DIRECTION ( 'NONE',  ( 1.000000000000000000, 0.000000000000000000, 0.000000000000000000 ) ) ;
#8485=VECTOR ( 'NONE', #553, 1000.000000000000000 ) ;
#8488=DIRECTION ( 'NONE',  ( 0.000000000000000000, -0.000000000000000000, 1.000000000000000000 ) ) ;
#8493=CARTESIAN_POINT ( 'NONE',  ( 5.000000000000000000, 50.00000000000000000, -27.54995462791182703 ) ) ;
#8527=ORIENTED_EDGE ( 'NONE', *, *, #12266, .T. ) ;
#8534=CYLINDRICAL_SURFACE ( 'NONE', #11909, 5.000000000000000000 ) ;
#8535=CARTESIAN_POINT ( 'NONE',  ( -0.6600000499078774174, 29.98375368882421910, 24.99348755773349140 ) ) ;
#8544=CARTESIAN_POINT ( 'NONE',  ( 3.429011039554510417E-15, 10.00000000000000000, 28.00000000000000355 ) ) ;
#8553=ADVANCED_FACE ( 'NONE', ( #10978 ), #10031, .F. ) ;
#8577=CARTESIAN_POINT ( 'NONE',  ( 10.00000000000000711, 20.65896320323604485, -22.91287847477919470 ) ) ;
#8585=CARTESIAN_POINT ( 'NONE',  ( -4.967261190099589108, 49.34148114543111774, 24.50164489405593571 ) ) ;
#8597=CARTESIAN_POINT ( 'NONE',  ( -5.000000000000000000, 50.00000000000000000, 24.49489742783178414 ) ) ;
#8599=VERTEX_POINT ( 'NONE', #8493 ) ;
#8600=EDGE_CURVE ( 'NONE', #10421, #6575, #36, .T. ) ;
#8617=CARTESIAN_POINT ( 'NONE',  ( 3.764190923162284985, 46.69295727064967849, 27.74679428998945596 ) ) ;
#8648=ORIENTED_EDGE ( 'NONE', *, *, #5893, .F. ) ;
#8655=DIRECTION ( 'NONE',  ( 0.000000000000000000, 0.000000000000000000, 1.000000000000000000 ) ) ;
#8658=CARTESIAN_POINT ( 'NONE',  ( -6.608338170980154302, 27.53359326989389189, 24.11557641055247458 ) ) ;
#8667=ORIENTED_EDGE ( 'NONE', *, *, #1107, .F. ) ;
#8672=ORIENTED_EDGE ( 'NONE', *, *, #6220, .T. ) ;
#8712=EDGE_LOOP ( 'NONE', ( #4094, #10451, #6984, #5288, #10655, #2957, #4678, #592, #11995, #5291, #4926, #4864, #983, #4535, #8667, #3193 ) ) ;
#8723=CARTESIAN_POINT ( 'NONE',  ( 8.675702521724353744, 25.01627270855146534, -26.62476894046449161 ) ) ;
#8727=CARTESIAN_POINT ( 'NONE',  ( 0.6566478411514924396, 54.96742651404818503, -27.99413128707798037 ) ) ;
#8732=ORIENTED_EDGE ( 'NONE', *, *, #1344, .F. ) ;
#8736=LINE ( 'NONE', #4872, #10877 ) ;
#8743=CARTESIAN_POINT ( 'NONE',  ( 2.610381677634093123, 10.34108370468245219, 24.86537221636008965 ) ) ;
#8759=( NAMED_UNIT ( * ) PLANE_ANGLE_UNIT ( ) SI_UNIT ( $, .RADIAN. ) );
#8761=CARTESIAN_POINT ( 'NONE',  ( 4.437260769980855279, 11.03236584733799930, -27.64772768517902790 ) ) ;
#8768=LINE ( 'NONE', #2176, #11319 ) ;
#8773=CARTESIAN_POINT ( 'NONE',  ( 0.000000000000000000, 0.000000000000000000, 0.000000000000000000 ) ) ;
#8776=CARTESIAN_POINT ( 'NONE',  ( -10.00000000000000355, 20.00000000000000355, -22.91287847477919826 ) ) ;
#8777=EDGE_CURVE ( 'NONE', #6575, #12211, #10555, .T. ) ;
#8778=CARTESIAN_POINT ( 'NONE',  ( -4.339203347172030156, 52.50587310092982563, -24.62124401584528499 ) ) ;
#8785=ADVANCED_FACE ( 'NONE', ( #5687 ), #8534, .F. ) ;
#8808=EDGE_CURVE ( 'NONE', #4258, #8883, #12161, .T. ) ;
#8813=CARTESIAN_POINT ( 'NONE',  ( 3.246557057937244029, 10.51899376542992925, -24.79585947768713439 ) ) ;
#8824=CARTESIAN_POINT ( 'NONE',  ( 6.607022230516116146, 12.46548842210657426, -27.21346531667574098 ) ) ;
#8825=B_SPLINE_CURVE_WITH_KNOTS ( 'NONE', 3,
 ( #375, #435, #3527, #8174, #1387, #10197, #2391, #11146, #2453, #9127, #4298, #12043, #6327, #11205, #4419, #1872, #8419, #5753, #6694, #10372, #1810, #4673, #10434, #1685, #9562, #11395, #9624, #8544 ),
 .UNSPECIFIED., .F., .F.,
 ( 4, 2, 2, 2, 2, 2, 2, 2, 2, 2, 2, 2, 2, 4 ),
 ( 0.03152606207563762863, 0.03251081260015469682, 0.03349556312467176500, 0.03546506417370590136, 0.03644981469822297648, 0.03743456522274005160, 0.03940406627177420185, 0.04038881679629127003, 0.04137356732080833821, 0.04235831784532541333, 0.04334306836984248845, 0.04531256941887662482, 0.04629731994339369994, 0.04728207046791076812 ),
 .UNSPECIFIED. ) ;
#8839=EDGE_LOOP ( 'NONE', ( #1019, #7765, #3561, #6101 ) ) ;
#8841=LINE ( 'NONE', #99, #10014 ) ;
#8846=CARTESIAN_POINT ( 'NONE',  ( 5.840594436583858240, 28.12365591114656738, -27.38546733845194936 ) ) ;
#8863=CARTESIAN_POINT ( 'NONE',  ( 0.6550203249928933102, 54.96765362015771927, 24.99347278016167095 ) ) ;
#8883=VERTEX_POINT ( 'NONE', #11825 ) ;
#8892=CARTESIAN_POINT ( 'NONE',  ( 5.297557166928031691, 11.51226837079426524, -27.49566921010548270 ) ) ;
#8903=CARTESIAN_POINT ( 'NONE',  ( 3.061616998149962604E-15, 10.00000000000000000, 25.00000000000000000 ) ) ;
#8924=CARTESIAN_POINT ( 'NONE',  ( 0.000000000000000000, -3.000000000000003109, 25.00000000000000355 ) ) ;
#8925=CARTESIAN_POINT ( 'NONE',  ( -5.017800233121429088, 11.34386344135788605, -24.49301625034288321 ) ) ;
#8929=VECTOR ( 'NONE', #3727, 1000.000000000000114 ) ;
#8933=DIRECTION ( 'NONE',  ( -0.000000000000000000, -1.000000000000000000, -0.000000000000000000 ) ) ;
#8935=CARTESIAN_POINT ( 'NONE',  ( 3.429011039554510417E-15, 10.00000000000000000, 28.00000000000000355 ) ) ;
#8937=CARTESIAN_POINT ( 'NONE',  ( -3.767190843690196633, 46.69628320461708171, 27.74639135108192534 ) ) ;
#8943=CARTESIAN_POINT ( 'NONE',  ( -3.767201726441450571, 53.30370413573731980, 24.71563014075751141 ) ) ;
#8957=ORIENTED_EDGE ( 'NONE', *, *, #10705, .F. ) ;
#8961=CARTESIAN_POINT ( 'NONE',  ( -3.975875746111922293, 46.95063182920211631, -27.71688932856698884 ) ) ;
#8973=CARTESIAN_POINT ( 'NONE',  ( -1.615502922434717492, 54.74315837822297937, -24.94959493428010688 ) ) ;
#8989=AXIS2_PLACEMENT_3D ( 'NONE', #11458, #2765, #8480 ) ;
#8991=B_SPLINE_CURVE_WITH_KNOTS ( 'NONE', 3,
 ( #9353, #8577, #12509, #9537, #10347, #10535, #4705, #3747, #9475, #6484, #716, #7502, #12323, #4520, #9415, #11372, #1664, #1725, #2801, #8395, #902, #10411, #5546, #4772, #7566, #10471, #2679, #9595 ),
 .UNSPECIFIED., .F., .F.,
 ( 4, 2, 2, 2, 2, 2, 2, 2, 2, 2, 2, 2, 2, 4 ),
 ( 0.04738924854463780201, 0.04936272659091893444, 0.05034946561405949372, 0.05133620463720005994, 0.05232294366034062616, 0.05330968268348119238, 0.05528316072976231788, 0.05626989975290288409, 0.05725663877604345031, 0.05923011682232458969, 0.06021685584546515591, 0.06120359486860571518, 0.06219033389174628140, 0.06317707291488684762 ),
 .UNSPECIFIED. ) ;
#8996=AXIS2_PLACEMENT_3D ( 'NONE', #8276, #474, #1368 ) ;
#9002=PRODUCT_DEFINITION_FORMATION_WITH_SPECIFIED_SOURCE ( 'ANY', '', #5993, .NOT_KNOWN. ) ;
#9021=AXIS2_PLACEMENT_3D ( 'NONE', #11433, #2744, #207 ) ;
#9037=CARTESIAN_POINT ( 'NONE',  ( -1.648736202249158733, 29.86860657404073294, 27.95327759174768190 ) ) ;
#9068=CARTESIAN_POINT ( 'NONE',  ( -3.766911610146119305, 46.69571375074811925, -24.71569286637712892 ) ) ;
#9070=CARTESIAN_POINT ( 'NONE',  ( -5.000000000000000000, 50.00000000000000000, 24.49489742783178414 ) ) ;
#9077=DIRECTION ( 'NONE',  ( -0.000000000000000000, -1.000000000000000000, -0.000000000000000000 ) ) ;
#9082=ORIENTED_EDGE ( 'NONE', *, *, #10377, .F. ) ;
#9091=EDGE_CURVE ( 'NONE', #8599, #11427, #11869, .T. ) ;
#9092=CARTESIAN_POINT ( 'NONE',  ( -2.212795773503799523, 45.51331203296545169, -27.91280268202237025 ) ) ;
#9101=CIRCLE ( 'NONE', #3609, 28.00000000000000000 ) ;
#9104=CARTESIAN_POINT ( 'NONE',  ( 4.147660976662388421, 10.89487115550369900, 27.69276736765331748 ) ) ;
#9105=CARTESIAN_POINT ( 'NONE',  ( 4.839017051182398887, 48.69964289075914365, -27.57876268693809507 ) ) ;
#9126=CARTESIAN_POINT ( 'NONE',  ( 0.000000000000000000, 0.000000000000000000, 0.000000000000000000 ) ) ;
#9127=CARTESIAN_POINT ( 'NONE',  ( -8.654264301703824103, 14.97889801067282889, 26.62950408590382168 ) ) ;
#9131=B_SPLINE_CURVE_WITH_KNOTS ( 'NONE', 3,
 ( #8474, #795, #5688, #4666, #1741, #6565, #7587, #5623, #9494, #1865, #11511, #2823, #1680, #11389, #6687, #8658, #5746, #4854, #10556, #9617, #925, #10367, #10613, #11452, #7710, #8535, #10430, #2699 ),
 .UNSPECIFIED., .F., .F.,
 ( 4, 2, 2, 2, 2, 2, 2, 2, 2, 2, 2, 2, 2, 4 ),
 ( 0.03159723681526421801, 0.03258403062298791120, 0.03357082443071160438, 0.03554441204615898381, 0.03653120585388267699, 0.03751799966160637018, 0.03850479346933006336, 0.03949158727705375654, 0.04146517489250114985, 0.04245196870022484303, 0.04343876250794853622, 0.04541235012339592259, 0.04639914393111962271, 0.04738593773884331589 ),
 .UNSPECIFIED. ) ;
#9132=CARTESIAN_POINT ( 'NONE',  ( -7.523754161084773351, 13.40468021027817791, -26.97107581164716095 ) ) ;
#9134=CARTESIAN_POINT ( 'NONE',  ( 4.142194555499470354, 10.89240068329948130, -27.69358117727547963 ) ) ;
#9140=CARTESIAN_POINT ( 'NONE',  ( 3.429011037612589670E-15, 0.000000000000000000, 28.00000000000000355 ) ) ;
#9163=CARTESIAN_POINT ( 'NONE',  ( -4.458389208371986712, 28.97542069971310141, 27.64960765936604759 ) ) ;
#9172=CARTESIAN_POINT ( 'NONE',  ( 9.660534914401177176, 22.60440596647124067, 26.28087847349582518 ) ) ;
#9195=CARTESIAN_POINT ( 'NONE',  ( -5.000000000000000000, 50.32679387323496911, 24.49489742783177704 ) ) ;
#9201=CARTESIAN_POINT ( 'NONE',  ( 7.946724766127979400, 13.89530605390606688, -23.70643652970303350 ) ) ;
#9218=CARTESIAN_POINT ( 'NONE',  ( 3.547335893868845513, 29.35536450536750408, 24.74892486337281738 ) ) ;
#9237=CARTESIAN_POINT ( 'NONE',  ( 0.000000000000000000, 0.000000000000000000, -28.00000000000000355 ) ) ;
#9240=CARTESIAN_POINT ( 'NONE',  ( 4.743537283058001819, 51.61420199850529400, -24.54618281552716041 ) ) ;
#9248=CARTESIAN_POINT ( 'NONE',  ( 5.000000000000000000, 50.00000000000000000, 24.49489742783178059 ) ) ;
#9256=EDGE_CURVE ( 'NONE', #6052, #1748, #7775, .T. ) ;
#9276=CARTESIAN_POINT ( 'NONE',  ( -4.493244791708733032, 52.21758165739003488, -27.63741816232653647 ) ) ;
#9281=CARTESIAN_POINT ( 'NONE',  ( 7.298955741910466699, 26.84326632351102759, 23.91197098918000918 ) ) ;
#9298=CARTESIAN_POINT ( 'NONE',  ( 3.061617023331388775E-15, 45.00000000000000711, 25.00000000000000000 ) ) ;
#9302=CARTESIAN_POINT ( 'NONE',  ( 4.493076325134499172, 52.21789521489533570, -24.59326131088672440 ) ) ;
#9306=DIRECTION ( 'NONE',  ( 0.000000000000000000, 0.000000000000000000, -1.000000000000000000 ) ) ;
#9312=CARTESIAN_POINT ( 'NONE',  ( 4.967437465254620932, 50.65784153438875848, 24.50160996501502098 ) ) ;
#9328=CARTESIAN_POINT ( 'NONE',  ( 3.303926766530076442, 46.23304915065238418, 24.78181020466353601 ) ) ;
#9353=CARTESIAN_POINT ( 'NONE',  ( 10.00000000000000355, 20.00000000000000355, -22.91287847477919826 ) ) ;
#9363=ORIENTED_EDGE ( 'NONE', *, *, #4811, .T. ) ;
#9388=CARTESIAN_POINT ( 'NONE',  ( 3.061617023331388775E-15, 45.00000000000000711, 25.00000000000000000 ) ) ;
#9415=CARTESIAN_POINT ( 'NONE',  ( 6.601689117734505174, 27.51820487403981375, -24.11400268645312650 ) ) ;
#9417=CARTESIAN_POINT ( 'NONE',  ( -3.294598684565033704E-22, 45.00000000000000711, -28.00000000000000355 ) ) ;
#9435=DIRECTION ( 'NONE',  ( 0.000000000000000000, 0.000000000000000000, -1.000000000000000000 ) ) ;
#9450=CARTESIAN_POINT ( 'NONE',  ( 0.000000000000000000, 70.00000000000000000, 0.000000000000000000 ) ) ;
#9451=CARTESIAN_POINT ( 'NONE',  ( 3.974960981574284347, 46.94936902441865101, 24.68265737646872893 ) ) ;
#9475=CARTESIAN_POINT ( 'NONE',  ( 8.964356567778166252, 24.44381301785154292, -23.33811713236289620 ) ) ;
#9485=DIRECTION ( 'NONE',  ( -0.000000000000000000, -0.000000000000000000, 1.000000000000000000 ) ) ;
#9494=CARTESIAN_POINT ( 'NONE',  ( -8.961327849752377617, 24.44988401922752530, 23.33927995079777062 ) ) ;
#9497=FACE_OUTER_BOUND ( 'NONE', #6130, .T. ) ;
#9498=STYLED_ITEM('',(#12591),#2064);
#9507=CIRCLE ( 'NONE', #7270, 25.00000000000000000 ) ;
#9514=DIRECTION ( 'NONE',  ( -0.000000000000000000, -0.000000000000000000, 1.000000000000000000 ) ) ;
#9537=CARTESIAN_POINT ( 'NONE',  ( 9.739799295956466096, 22.29052955100696920, -23.02479834983350671 ) ) ;
#9539=CARTESIAN_POINT ( 'NONE',  ( 2.216731485194162854, 45.50631650129702166, -27.91375863587312267 ) ) ;
#9544=CARTESIAN_POINT ( 'NONE',  ( -1.613768212969407978, 45.25637963430527577, -27.95508518501520001 ) ) ;
#9562=CARTESIAN_POINT ( 'NONE',  ( -1.322843585767942365, 10.08231100245556000, 27.97069189717537796 ) ) ;
#9575=CARTESIAN_POINT ( 'NONE',  ( 3.971194329084580588, 46.94417401791325517, 27.71757479093061249 ) ) ;
#9586=EDGE_CURVE ( 'NONE', #7533, #6436, #3849, .T. ) ;
#9592=CARTESIAN_POINT ( 'NONE',  ( -8.965892573770299023, 24.44066166037483612, -26.52619932659681012 ) ) ;
#9595=CARTESIAN_POINT ( 'NONE',  ( -3.709758735690515970E-18, 30.00000000000001066, -25.00000000000000000 ) ) ;
#9597=CARTESIAN_POINT ( 'NONE',  ( 3.974870633954390886, 46.94939079583478048, -27.71703188956191255 ) ) ;
#9605=EDGE_LOOP ( 'NONE', ( #126, #6235, #3870, #10782, #4255, #5631, #4195, #4893, #1105, #11303, #4333, #5542, #1443, #3126, #7512, #8065 ) ) ;
#9617=CARTESIAN_POINT ( 'NONE',  ( -4.448741964560915640, 28.96190946584970405, 24.60274125495980613 ) ) ;
#9624=CARTESIAN_POINT ( 'NONE',  ( -0.3293999078206490405, 9.999999999999992895, 28.00000000000000000 ) ) ;
#9638=ADVANCED_FACE ( 'NONE', ( #1067 ), #3027, .F. ) ;
#9641=CARTESIAN_POINT ( 'NONE',  ( 1.314997555680467389, 10.06486170053814533, 24.97384176433527969 ) ) ;
#9657=DIRECTION ( 'NONE',  ( 0.000000000000000000, 0.000000000000000000, -1.000000000000000000 ) ) ;
#9669=DIRECTION ( 'NONE',  ( -0.000000000000000000, -1.000000000000000000, -0.000000000000000000 ) ) ;
#9682=CARTESIAN_POINT ( 'NONE',  ( -0.6587806068097139534, 54.96719481440166533, 27.99408942736936012 ) ) ;
#9683=CARTESIAN_POINT ( 'NONE',  ( 7.533473311303588993, 26.60795856157748673, -26.97164952521862702 ) ) ;
#9686=DIRECTION ( 'NONE',  ( 0.000000000000000000, 1.000000000000000000, 0.000000000000000000 ) ) ;
#9698=CARTESIAN_POINT ( 'NONE',  ( 3.764997658848628692, 46.69378447153945189, -24.71596740620162436 ) ) ;
#9703=CARTESIAN_POINT ( 'NONE',  ( 7.514434402675104430, 13.39403693888593772, 23.84492327520115396 ) ) ;
#9735=CARTESIAN_POINT ( 'NONE',  ( -0.6638428588095105498, 10.01651532611708895, 24.99338002059894137 ) ) ;
#9751=VERTEX_POINT ( 'NONE', #6953 ) ;
#9754=UNCERTAINTY_MEASURE_WITH_UNIT (LENGTH_MEASURE( 1.000000000000000082E-05 ), #11010, 'distance_accuracy_value', 'NONE');
#9759=CARTESIAN_POINT ( 'NONE',  ( 1.614235646224727372, 54.74352724365349587, 24.94966740611544509 ) ) ;
#9767=CARTESIAN_POINT ( 'NONE',  ( 7.192769615190809278E-19, 10.00000000000000000, -28.00000000000000355 ) ) ;
#9774=CARTESIAN_POINT ( 'NONE',  ( 1.317448503741515342, 10.08163033484836113, -24.96744191981147409 ) ) ;
#9781=CARTESIAN_POINT ( 'NONE',  ( 4.338316237973660172, 52.50713254139536446, 27.66247836308076558 ) ) ;
#9789=CARTESIAN_POINT ( 'NONE',  ( -0.3267093297687971853, 45.00000000000001421, -28.00000000000001421 ) ) ;
#9800=EDGE_CURVE ( 'NONE', #5412, #6224, #7142, .T. ) ;
#9802=CARTESIAN_POINT ( 'NONE',  ( 3.429011039554510417E-15, 10.00000000000000000, 28.00000000000000355 ) ) ;
#9803=CARTESIAN_POINT ( 'NONE',  ( -3.307156092220256749, 53.76411647547837447, -24.78137765757908895 ) ) ;
#9810=CARTESIAN_POINT ( 'NONE',  ( 8.982292369834492973, 24.44317814053119875, -26.52147360909799545 ) ) ;
#9814=ORIENTED_EDGE ( 'NONE', *, *, #12427, .F. ) ;
#9825=AXIS2_PLACEMENT_3D ( 'NONE', #7717, #9686, #11337 ) ;
#9831=ORIENTED_EDGE ( 'NONE', *, *, #9586, .T. ) ;
#9847=CARTESIAN_POINT ( 'NONE',  ( 1.297896323713631617, 54.83982511471705834, 27.97176989401758362 ) ) ;
#9863=EDGE_LOOP ( 'NONE', ( #6098, #8672, #11240, #11939, #11717, #2816 ) ) ;
#9872=CARTESIAN_POINT ( 'NONE',  ( -1.300368161224497943, 54.83901424438912642, 27.97162986671915874 ) ) ;
#9873=CARTESIAN_POINT ( 'NONE',  ( 6.847974502850965983, 27.29450679136124691, -27.15070937874627788 ) ) ;
#9881=VECTOR ( 'NONE', #4614, 1000.000000000000000 ) ;
#9882=LINE ( 'NONE', #8211, #7180 ) ;
#9893=CARTESIAN_POINT ( 'NONE',  ( -4.329834338986901621, 47.49413952373966197, -24.62232128246942509 ) ) ;
#9901=CIRCLE ( 'NONE', #4021, 25.00000000000000000 ) ;
#9902=CARTESIAN_POINT ( 'NONE',  ( 7.537524037383855458, 13.39612119810769819, -23.84148986838564710 ) ) ;
#9912=SHAPE_REPRESENTATION_RELATIONSHIP ( 'NONE' , 'NONE' ,  #4339, #12311 ) ;
#9924=CARTESIAN_POINT ( 'NONE',  ( -1.652347697333065968, 10.13198208422932467, 24.94742907234073215 ) ) ;
#9946=DIRECTION ( 'NONE',  ( -0.000000000000000000, -0.000000000000000000, 1.000000000000000000 ) ) ;
#9948=CARTESIAN_POINT ( 'NONE',  ( 1.295572856795887295, 54.84026084924703071, 24.96846459459551681 ) ) ;
#9962=CARTESIAN_POINT ( 'NONE',  ( -3.306342958134543153, 53.76488593550792672, 24.78149064010515445 ) ) ;
#9974=ORIENTED_EDGE ( 'NONE', *, *, #3645, .T. ) ;
#9977=CARTESIAN_POINT ( 'NONE',  ( -3.307119090283400897, 53.76412354891344592, -27.80497456210996887 ) ) ;
#9998=CARTESIAN_POINT ( 'NONE',  ( 9.353276081244219498, 23.55311451265283296, 23.18479875781715194 ) ) ;
#10006=VERTEX_POINT ( 'NONE', #12053 ) ;
#10014=VECTOR ( 'NONE', #4981, 1000.000000000000000 ) ;
#10018=CARTESIAN_POINT ( 'NONE',  ( -1.609496042995007370, 45.26329109710995624, 27.95414474166305041 ) ) ;
#10023=CARTESIAN_POINT ( 'NONE',  ( -9.983620353272891990, 19.33838559509563026, -26.15967447858658090 ) ) ;
#10031=CYLINDRICAL_SURFACE ( 'NONE', #3591, 5.000000000000000000 ) ;
#10053=CARTESIAN_POINT ( 'NONE',  ( -9.983885927020196505, 20.65630489035274664, 26.15957239041219395 ) ) ;
#10057=CARTESIAN_POINT ( 'NONE',  ( 5.000000000000000000, 50.00000000000000000, -27.54995462791182703 ) ) ;
#10061=CARTESIAN_POINT ( 'NONE',  ( 3.543374587579615209, 29.35684306698988877, 27.77654735269002018 ) ) ;
#10062=DIRECTION ( 'NONE',  ( -0.000000000000000000, -1.000000000000000000, -0.000000000000000000 ) ) ;
#10071=VECTOR ( 'NONE', #6890, 1000.000000000000000 ) ;
#10080=DIRECTION ( 'NONE',  ( -0.000000000000000000, -0.000000000000000000, 1.000000000000000000 ) ) ;
#10082=CARTESIAN_POINT ( 'NONE',  ( -4.968274749745848595, 50.65218571871033504, 24.50144017370611493 ) ) ;
#10083=CARTESIAN_POINT ( 'NONE',  ( 10.00000000000000178, 19.67085183536559967, -26.15339366124404208 ) ) ;
#10090=DIRECTION ( 'NONE',  ( 0.000000000000000000, 0.000000000000000000, -1.000000000000000000 ) ) ;
#10099=EDGE_CURVE ( 'NONE', #1748, #9751, #3784, .T. ) ;
#10111=CARTESIAN_POINT ( 'NONE',  ( -6.609692946276023662, 12.48878433695339218, 24.11181729628509984 ) ) ;
#10124=DIRECTION ( 'NONE',  ( -0.000000000000000000, -1.000000000000000000, -0.000000000000000000 ) ) ;
#10144=CARTESIAN_POINT ( 'NONE',  ( -9.868592978625752465, 18.35130037890183985, -26.20335131078380897 ) ) ;
#10157=ADVANCED_FACE ( 'NONE', ( #11529 ), #7536, .T. ) ;
#10171=CARTESIAN_POINT ( 'NONE',  ( -6.851336394414588860, 12.70864359358585460, 24.04404201862471524 ) ) ;
#10173=CARTESIAN_POINT ( 'NONE',  ( -1.322605739864947116, 29.91771837663726785, 27.97070232718573735 ) ) ;
#10176=ADVANCED_FACE ( 'NONE', ( #3596 ), #1883, .T. ) ;
#10181=CARTESIAN_POINT ( 'NONE',  ( 2.606202220541010028, 29.66002383724781311, 27.88024221855608431 ) ) ;
#10197=CARTESIAN_POINT ( 'NONE',  ( -9.674627460180301952, 17.38490666077015590, 26.27586073059115535 ) ) ;
#10229=VERTEX_POINT ( 'NONE', #5065 ) ;
#10234=CARTESIAN_POINT ( 'NONE',  ( 3.429011037612589670E-15, 0.000000000000000000, 28.00000000000000355 ) ) ;
#10240=CARTESIAN_POINT ( 'NONE',  ( 8.125441273627673766, 25.83810069393247488, 26.79577025665707879 ) ) ;
#10242=ORIENTED_EDGE ( 'NONE', *, *, #11183, .F. ) ;
#10258=ADVANCED_FACE ( 'NONE', ( #3154 ), #11781, .F. ) ;
#10270=VERTEX_POINT ( 'NONE', #5824 ) ;
#10339=CARTESIAN_POINT ( 'NONE',  ( 4.149575074854375600, 29.10425525072577102, 24.65509887497819008 ) ) ;
#10347=CARTESIAN_POINT ( 'NONE',  ( 9.658351069856484727, 22.61227114741398836, -23.05920763558311037 ) ) ;
#10349=CARTESIAN_POINT ( 'NONE',  ( 9.933941257241759359, 18.67913347266169666, 26.17891498049026211 ) ) ;
#10365=CARTESIAN_POINT ( 'NONE',  ( 0.000000000000000000, 50.00000000000000000, -28.00000000000000711 ) ) ;
#10367=CARTESIAN_POINT ( 'NONE',  ( -3.243418093453738216, 29.48203249043655561, 24.79625640031606082 ) ) ;
#10372=CARTESIAN_POINT ( 'NONE',  ( -4.446180375167638310, 11.03685037693071891, 27.64627648346033340 ) ) ;
#10377=EDGE_CURVE ( 'NONE', #11047, #3445, #8736, .T. ) ;
#10383=EDGE_CURVE ( 'NONE', #6436, #10421, #4762, .T. ) ;
#10397=EDGE_CURVE ( 'NONE', #6466, #3859, #7143, .T. ) ;
#10409=CARTESIAN_POINT ( 'NONE',  ( -3.230287074538311654, 29.46960489198576383, -27.81483967107842403 ) ) ;
#10411=CARTESIAN_POINT ( 'NONE',  ( 2.611671490993349831, 29.65850121673988227, -24.86521292532985328 ) ) ;
#10421=VERTEX_POINT ( 'NONE', #9248 ) ;
#10423=EDGE_LOOP ( 'NONE', ( #860, #6148, #4000, #1031, #7042, #2545, #5482, #10608, #8527, #11220, #10489, #8648, #5057, #5348, #3082, #7306 ) ) ;
#10430=CARTESIAN_POINT ( 'NONE',  ( -0.3295322344531997905, 30.00000000000001066, 25.00000000000001066 ) ) ;
#10434=CARTESIAN_POINT ( 'NONE',  ( -2.612894974895984213, 10.32515758870095546, 27.88526400371763003 ) ) ;
#10446=CARTESIAN_POINT ( 'NONE',  ( 4.338021161404794768, 47.49236434914906368, 24.62144314154611990 ) ) ;
#10450=CARTESIAN_POINT ( 'NONE',  ( 3.429011037612589276E-15, 67.00000000000000000, 28.00000000000000000 ) ) ;
#10451=ORIENTED_EDGE ( 'NONE', *, *, #5410, .T. ) ;
#10471=CARTESIAN_POINT ( 'NONE',  ( 0.6684871184501431918, 29.98311267939276092, -24.99323153604321490 ) ) ;
#10489=ORIENTED_EDGE ( 'NONE', *, *, #9256, .F. ) ;
#10490=CARTESIAN_POINT ( 'NONE',  ( -8.980220477185385519, 24.44733350940715866, -23.33298399582670157 ) ) ;
#10502=ORIENTED_EDGE ( 'NONE', *, *, #9256, .T. ) ;
#10511=DIRECTION ( 'NONE',  ( 0.000000000000000000, 0.000000000000000000, -1.000000000000000000 ) ) ;
#10513=CARTESIAN_POINT ( 'NONE',  ( 4.741665211587190676, 48.38057902784014175, 27.59588127970951632 ) ) ;
#10514=CARTESIAN_POINT ( 'NONE',  ( 4.450527323037263727, 11.02130320606087821, 24.60818795580814822 ) ) ;
#10532=CARTESIAN_POINT ( 'NONE',  ( -4.140053538423851224E-16, 30.00000000000001066, -28.00000000000000355 ) ) ;
#10535=CARTESIAN_POINT ( 'NONE',  ( 9.466290622766221574, 23.23991477998078636, -23.13871526284164304 ) ) ;
#10554=CARTESIAN_POINT ( 'NONE',  ( 0.000000000000000000, -3.000000000000003109, 0.000000000000000000 ) ) ;
#10555=LINE ( 'NONE', #12285, #3397 ) ;
#10556=CARTESIAN_POINT ( 'NONE',  ( -5.025242304149237782, 28.65182443915274746, 24.49149081028624053 ) ) ;
#10559=CARTESIAN_POINT ( 'NONE',  ( 28.00000000000000711, -3.000000000000003109, 0.000000000000000000 ) ) ;
#10561=CARTESIAN_POINT ( 'NONE',  ( 4.968243444659302455, 50.65191788982895815, -27.55577634755498906 ) ) ;
#10570=CARTESIAN_POINT ( 'NONE',  ( 0.000000000000000000, 0.000000000000000000, 0.000000000000000000 ) ) ;
#10591=EDGE_CURVE ( 'NONE', #11427, #1348, #2944, .T. ) ;
#10592=CARTESIAN_POINT ( 'NONE',  ( 0.000000000000000000, 67.00000000000000000, -28.00000000000000000 ) ) ;
#10601=DIRECTION ( 'NONE',  ( -0.000000000000000000, -0.000000000000000000, 1.000000000000000000 ) ) ;
#10608=ORIENTED_EDGE ( 'NONE', *, *, #8399, .T. ) ;
#10613=CARTESIAN_POINT ( 'NONE',  ( -2.619138840591237472, 29.67330545628644600, 24.87083797681799169 ) ) ;
#10624=CARTESIAN_POINT ( 'NONE',  ( -5.000000000000000000, 50.00000000000000000, -27.54995462791182703 ) ) ;
#10627=CIRCLE ( 'NONE', #5175, 25.00000000000000355 ) ;
#10640=CARTESIAN_POINT ( 'NONE',  ( 9.465993554759519313, 16.75899710733777326, 23.13883973029316010 ) ) ;
#10655=ORIENTED_EDGE ( 'NONE', *, *, #10591, .F. ) ;
#10675=CARTESIAN_POINT ( 'NONE',  ( -9.935193375007562722, 21.31442233758455274, -22.94148538850174646 ) ) ;
#10689=ORIENTED_EDGE ( 'NONE', *, *, #12508, .T. ) ;
#10702=CARTESIAN_POINT ( 'NONE',  ( 6.110979747148361341, 12.05740682582580625, 24.24803741642852373 ) ) ;
#10705=EDGE_CURVE ( 'NONE', #4669, #10800, #7604, .T. ) ;
#10723=CARTESIAN_POINT ( 'NONE',  ( 0.3282094658107080343, 10.00000000000000000, -28.00000000000000355 ) ) ;
#10738=CARTESIAN_POINT ( 'NONE',  ( -6.849710128414980836, 27.29284600759404356, -24.04449974210336904 ) ) ;
#10744=CARTESIAN_POINT ( 'NONE',  ( 6.104805980962106915, 27.92701719664820459, -27.32760709691111956 ) ) ;
#10766=CARTESIAN_POINT ( 'NONE',  ( -4.146808533202904989, 10.89445667252602945, -27.69290272286349364 ) ) ;
#10782=ORIENTED_EDGE ( 'NONE', *, *, #2085, .F. ) ;
#10800=VERTEX_POINT ( 'NONE', #3028 ) ;
#10808=CARTESIAN_POINT ( 'NONE',  ( 1.321572630236863111, 29.93396655346517576, -27.97622437266944928 ) ) ;
#10820=CARTESIAN_POINT ( 'NONE',  ( -7.514688383768903357, 13.39426057884744026, -23.84485093628785535 ) ) ;
#10825=CARTESIAN_POINT ( 'NONE',  ( 0.000000000000000000, 67.00000000000000000, 0.000000000000000000 ) ) ;
#10831=CARTESIAN_POINT ( 'NONE',  ( -4.744081181139592651, 48.38712208294071360, -24.54608042500704457 ) ) ;
#10838=B_SPLINE_CURVE_WITH_KNOTS ( 'NONE', 3,
 ( #3684, #11431, #2742, #2163, #5089, #205, #2927, #3112, #9781, #11805, #7812, #3999, #269, #3053, #967, #8005, #9847, #7749, #3938, #1969 ),
 .UNSPECIFIED., .F., .F.,
 ( 4, 2, 2, 2, 2, 2, 2, 2, 2, 4 ),
 ( 0.000000000000000000, 0.0009792184361842109445, 0.001468827654276316742, 0.001958436872368422756, 0.002937655308552634351, 0.003916873744736846380, 0.004896092180921057975, 0.005875310617105269570, 0.006854529053289482032, 0.007833747489473694495 ),
 .UNSPECIFIED. ) ;
#10851=DIRECTION ( 'NONE',  ( -0.000000000000000000, -1.000000000000000000, -0.000000000000000000 ) ) ;
#10856=CARTESIAN_POINT ( 'NONE',  ( 0.3301019608631527991, 45.00000000000000711, 28.00000000000000711 ) ) ;
#10857=CARTESIAN_POINT ( 'NONE',  ( 9.868636702206156741, 18.35145658115177980, -26.20333517057690997 ) ) ;
#10867=CARTESIAN_POINT ( 'NONE',  ( -0.3301927727158289749, 10.00000000000000000, 25.00000000000000355 ) ) ;
#10870=B_SPLINE_CURVE_WITH_KNOTS ( 'NONE', 3,
 ( #4858, #11581, #10808, #5115, #6880, #4026, #6001, #3140, #6751, #8846, #10744, #3899, #9873, #9683, #993, #8723, #9810, #2056, #38, #5052, #1121, #4089, #7011, #7777 ),
 .UNSPECIFIED., .F., .F.,
 ( 4, 2, 2, 2, 2, 2, 2, 2, 2, 2, 2, 4 ),
 ( 9.545105710734825969E-19, 0.001971105590603967981, 0.002956658385905950020, 0.003942211181207931625, 0.005913316771811892233, 0.006898869567113871670, 0.007884422362415852842, 0.009855527953019816920, 0.01182663354362378100, 0.01281218633892575870, 0.01379773913422773640, 0.01576884472483168140 ),
 .UNSPECIFIED. ) ;
#10877=VECTOR ( 'NONE', #50, 1000.000000000000000 ) ;
#10881=DIRECTION ( 'NONE',  ( -0.000000000000000000, -1.000000000000000000, -0.000000000000000000 ) ) ;
#10892=CARTESIAN_POINT ( 'NONE',  ( -7.929079634139357680, 13.89786668772332767, -23.71027527960010417 ) ) ;
#10897=CARTESIAN_POINT ( 'NONE',  ( 3.975724277407679974, 46.95046481276702366, -24.68253032026751370 ) ) ;
#10900=CARTESIAN_POINT ( 'NONE',  ( -4.247064150047941133, 47.35626993272530427, 27.67617995880919324 ) ) ;
#10913=DIRECTION ( 'NONE',  ( -0.000000000000000000, -0.000000000000000000, 1.000000000000000000 ) ) ;
#10946=CARTESIAN_POINT ( 'NONE',  ( 9.740751885065668247, 22.28587776697542466, 26.25114245506233601 ) ) ;
#10948=CARTESIAN_POINT ( 'NONE',  ( -1.300905012451813336, 45.16112489716824996, 24.96819491493427634 ) ) ;
#10957=CARTESIAN_POINT ( 'NONE',  ( -9.673467176944807733, 17.38163042592174889, -23.05306748635229752 ) ) ;
#10973=CARTESIAN_POINT ( 'NONE',  ( -2.508190414677843982, 54.33763061856527088, 24.87535316732256163 ) ) ;
#10978=FACE_OUTER_BOUND ( 'NONE', #11891, .T. ) ;
#10990=CARTESIAN_POINT ( 'NONE',  ( -4.871678679536868728, 48.86275246128555239, -27.57295404460982269 ) ) ;
#11006=CARTESIAN_POINT ( 'NONE',  ( 8.977351811841533191, 24.45372485761732761, 26.52316716509305294 ) ) ;
#11010=( LENGTH_UNIT ( ) NAMED_UNIT ( * ) SI_UNIT ( .MILLI., .METRE. ) );
#11015=CARTESIAN_POINT ( 'NONE',  ( -1.314141907159803946, 10.08123752450589095, -24.96759818712484957 ) ) ;
#11019=CARTESIAN_POINT ( 'NONE',  ( -10.00000000000000355, 20.00000000000000355, -28.00000000000000711 ) ) ;
#11025=CARTESIAN_POINT ( 'NONE',  ( -1.137267047700306843, 45.12832572938893350, 27.97735201090558732 ) ) ;
#11028=CARTESIAN_POINT ( 'NONE',  ( -4.555463605440090546, 47.93247208080379806, -24.58153461361902359 ) ) ;
#11047=VERTEX_POINT ( 'NONE', #8597 ) ;
#11064=CARTESIAN_POINT ( 'NONE',  ( 9.357362328184084532, 16.45777577070792219, 26.39048341541894871 ) ) ;
#11065=CARTESIAN_POINT ( 'NONE',  ( 4.484841213128739845, 47.78346385583337508, -27.63860224454065317 ) ) ;
#11071=CARTESIAN_POINT ( 'NONE',  ( -1.002883791299520887E-19, 10.00000000000000000, -25.00000000000000000 ) ) ;
#11081=CARTESIAN_POINT ( 'NONE',  ( 4.337826254667723092, 52.50833866356535395, 24.62149076657007640 ) ) ;
#11085=DIRECTION ( 'NONE',  ( -0.000000000000000000, -1.000000000000000000, -0.000000000000000000 ) ) ;
#11090=CARTESIAN_POINT ( 'NONE',  ( -4.839306774598123084, 51.30008082132634684, 24.52723862394605092 ) ) ;
#11118=CARTESIAN_POINT ( 'NONE',  ( -6.106142575418606278, 12.07400325324896784, 24.24423224237354901 ) ) ;
#11131=VECTOR ( 'NONE', #534, 1000.000000000000000 ) ;
#11132=CARTESIAN_POINT ( 'NONE',  ( -2.217326200926027724, 45.51555228448187762, 24.90189708455264395 ) ) ;
#11143=LINE ( 'NONE', #12101, #8485 ) ;
#11144=VECTOR ( 'NONE', #3682, 1000.000000000000000 ) ;
#11146=CARTESIAN_POINT ( 'NONE',  ( -9.106176344275144885, 15.85459820044763823, 26.47820341525681442 ) ) ;
#11181=CARTESIAN_POINT ( 'NONE',  ( -9.106574839427329593, 15.85560948713796492, 23.28279145951148266 ) ) ;
#11183=EDGE_CURVE ( 'NONE', #6466, #4258, #4088, .T. ) ;
#11194=VERTEX_POINT ( 'NONE', #1929 ) ;
#11205=CARTESIAN_POINT ( 'NONE',  ( -6.840285088253086343, 12.69813275654655094, 27.15267049763187401 ) ) ;
#11210=EDGE_CURVE ( 'NONE', #6725, #3445, #1882, .T. ) ;
#11220=ORIENTED_EDGE ( 'NONE', *, *, #10099, .F. ) ;
#11233=EDGE_CURVE ( 'NONE', #2882, #6159, #7256, .T. ) ;
#11234=CARTESIAN_POINT ( 'NONE',  ( 6.611279324052055095, 27.53068265742442122, 24.11471400905219298 ) ) ;
#11240=ORIENTED_EDGE ( 'NONE', *, *, #3273, .T. ) ;
#11241=CARTESIAN_POINT ( 'NONE',  ( -6.605663331672668726, 27.51475609591144789, 27.21088142802653920 ) ) ;
#11269=DIRECTION ( 'NONE',  ( 0.000000000000000000, -1.000000000000000000, -0.000000000000000000 ) ) ;
#11303=ORIENTED_EDGE ( 'NONE', *, *, #2188, .T. ) ;
#11307=EDGE_CURVE ( 'NONE', #12230, #6159, #4315, .T. ) ;
#11308=CARTESIAN_POINT ( 'NONE',  ( -1.320906402760432918, 29.93395141324767295, -27.97622082073361227 ) ) ;
#11319=VECTOR ( 'NONE', #1915, 1000.000000000000000 ) ;
#11320=ORIENTED_EDGE ( 'NONE', *, *, #5045, .F. ) ;
#11330=AXIS2_PLACEMENT_3D ( 'NONE', #10559, #11269, #9435 ) ;
#11337=DIRECTION ( 'NONE',  ( 0.000000000000000000, 0.000000000000000000, -1.000000000000000000 ) ) ;
#11354=CARTESIAN_POINT ( 'NONE',  ( 9.659257073854845999, 17.39080730681331488, 23.05883108104414347 ) ) ;
#11364=CARTESIAN_POINT ( 'NONE',  ( 9.983143436873248788, 20.66859359106200955, 22.92025639428880623 ) ) ;
#11372=CARTESIAN_POINT ( 'NONE',  ( 6.099398173400666145, 27.93114403207803420, -24.24592268179950594 ) ) ;
#11381=CARTESIAN_POINT ( 'NONE',  ( -3.304393266822325703, 46.23318141187127139, 24.78176792680001839 ) ) ;
#11382=ORIENTED_EDGE ( 'NONE', *, *, #796, .F. ) ;
#11388=CARTESIAN_POINT ( 'NONE',  ( -1.297374591076399408, 54.83977433137422253, -24.96837001061641104 ) ) ;
#11389=CARTESIAN_POINT ( 'NONE',  ( -7.519134213638725583, 26.60056234660722652, 23.84343405217310874 ) ) ;
#11394=CARTESIAN_POINT ( 'NONE',  ( 3.061617454482527662E-15, 30.00000000000001066, 25.00000000000000000 ) ) ;
#11395=CARTESIAN_POINT ( 'NONE',  ( -0.6613819929564737077, 10.01636118122183028, 27.99414392723079459 ) ) ;
#11427=VERTEX_POINT ( 'NONE', #6432 ) ;
#11431=CARTESIAN_POINT ( 'NONE',  ( 5.000000000000000000, 50.33115875943847328, 27.54995462791182348 ) ) ;
#11433=CARTESIAN_POINT ( 'NONE',  ( 0.000000000000000000, 0.000000000000000000, 0.000000000000000000 ) ) ;
#11449=CARTESIAN_POINT ( 'NONE',  ( -7.946065455725393356, 26.10639172058064972, -23.70672747870507280 ) ) ;
#11452=CARTESIAN_POINT ( 'NONE',  ( -1.651830483015944262, 29.86811216670179903, 24.94746627493933744 ) ) ;
#11456=ORIENTED_EDGE ( 'NONE', *, *, #3248, .T. ) ;
#11457=CARTESIAN_POINT ( 'NONE',  ( 2.507195821380045153, 54.33828039948598843, -27.88885893167862662 ) ) ;
#11458=CARTESIAN_POINT ( 'NONE',  ( 0.000000000000000000, 50.00000000000000000, -28.00000000000000711 ) ) ;
#11472=CARTESIAN_POINT ( 'NONE',  ( 5.000000000000000000, 49.66912405214284831, 27.54995462791181637 ) ) ;
#11509=FACE_OUTER_BOUND ( 'NONE', #1231, .T. ) ;
#11511=CARTESIAN_POINT ( 'NONE',  ( -8.483825669166648709, 25.30371668182424827, 23.51725424962153355 ) ) ;
#11527=CLOSED_SHELL ( 'NONE', ( #7541, #6912, #8785, #11864, #4982, #2710, #11924, #10176, #10157, #5744, #12110, #3735, #10258, #4914, #8275, #9638, #8553, #333 ) ) ;
#11529=FACE_OUTER_BOUND ( 'NONE', #1111, .T. ) ;
#11540=CARTESIAN_POINT ( 'NONE',  ( -5.023203578122774182, 11.34694221345378828, -27.54729890636757261 ) ) ;
#11555=CARTESIAN_POINT ( 'NONE',  ( -9.105758978599869380, 24.14626203848898101, -26.47834574479485070 ) ) ;
#11556=ORIENTED_EDGE ( 'NONE', *, *, #3765, .T. ) ;
#11568=EDGE_CURVE ( 'NONE', #6113, #10800, #90, .T. ) ;
#11581=CARTESIAN_POINT ( 'NONE',  ( 0.6668850494917962779, 30.00000000000000355, -28.00000000000000711 ) ) ;
#11583=ORIENTED_EDGE ( 'NONE', *, *, #4810, .T. ) ;
#11584=CARTESIAN_POINT ( 'NONE',  ( 1.609999862365107504, 54.73655139282131898, -27.95411785540357030 ) ) ;
#11596=CARTESIAN_POINT ( 'NONE',  ( 1.300123024442352504, 45.16070347875686508, -24.96827571664099565 ) ) ;
#11597=FACE_OUTER_BOUND ( 'NONE', #11771, .T. ) ;
#11599=CARTESIAN_POINT ( 'NONE',  ( 4.491735821183317157, 47.77958954773085765, 27.63766201934051026 ) ) ;
#11600=CARTESIAN_POINT ( 'NONE',  ( 5.022951428105686844, 11.32827475346531720, 24.49655794125914099 ) ) ;
#11601=ORIENTED_EDGE ( 'NONE', *, *, #12266, .F. ) ;
#11632=DIRECTION ( 'NONE',  ( 1.000000000000000000, 0.000000000000000000, 0.000000000000000000 ) ) ;
#11638=ORIENTED_EDGE ( 'NONE', *, *, #796, .T. ) ;
#11646=CARTESIAN_POINT ( 'NONE',  ( -0.3267839603878587851, 54.99999999999999289, 28.00000000000000355 ) ) ;
#11653=CARTESIAN_POINT ( 'NONE',  ( 3.061616998149962604E-15, 10.00000000000000000, 25.00000000000000000 ) ) ;
#11661=DIRECTION ( 'NONE',  ( -0.000000000000000000, -1.000000000000000000, -0.000000000000000000 ) ) ;
#11664=CARTESIAN_POINT ( 'NONE',  ( 4.491542451266983704, 47.77873343313099497, -24.59354576118897739 ) ) ;
#11667=CARTESIAN_POINT ( 'NONE',  ( 4.967476492172508529, 49.34237399800478840, 27.55591537130747426 ) ) ;
#11668=VECTOR ( 'NONE', #8175, 1000.000000000000000 ) ;
#11682=CYLINDRICAL_SURFACE ( 'NONE', #2432, 25.00000000000000000 ) ;
#11701=CARTESIAN_POINT ( 'NONE',  ( -1.324565580760808992, 29.93364609169914914, -24.97324923543901320 ) ) ;
#11717=ORIENTED_EDGE ( 'NONE', *, *, #3248, .F. ) ;
#11740=CARTESIAN_POINT ( 'NONE',  ( 5.029111531688879921, 11.35041964440615914, -24.49069713376460555 ) ) ;
#11745=ORIENTED_EDGE ( 'NONE', *, *, #12357, .T. ) ;
#11749=CARTESIAN_POINT ( 'NONE',  ( 5.015793544112643332, 11.34265857438676939, -27.54864687089846598 ) ) ;
#11759=DIRECTION ( 'NONE',  ( -0.000000000000000000, -1.000000000000000000, -0.000000000000000000 ) ) ;
#11763=CARTESIAN_POINT ( 'NONE',  ( 5.018193169041119006, 11.34410162984384840, 27.54819609062873198 ) ) ;
#11771=EDGE_LOOP ( 'NONE', ( #7597, #882, #4075, #2077, #11954, #10502 ) ) ;
#11781=CYLINDRICAL_SURFACE ( 'NONE', #4197, 25.00000000000000000 ) ;
#11789=CARTESIAN_POINT ( 'NONE',  ( 3.241086154805254083, 10.53405487867120982, 24.79105057270042067 ) ) ;
#11791=CARTESIAN_POINT ( 'NONE',  ( -1.643232170762119360, 10.13039557248869471, -27.95362914149064437 ) ) ;
#11794=FACE_OUTER_BOUND ( 'NONE', #138, .T. ) ;
#11800=ORIENTED_EDGE ( 'NONE', *, *, #3016, .F. ) ;
#11805=CARTESIAN_POINT ( 'NONE',  ( 3.975249800407504974, 53.05026070773460134, 27.71698190627791192 ) ) ;
#11825=CARTESIAN_POINT ( 'NONE',  ( -5.000000000000000000, 50.00000000000000000, -24.49489742783178059 ) ) ;
#11832=CARTESIAN_POINT ( 'NONE',  ( -4.744286179476278953, 51.61208845373312926, 27.59543232531387247 ) ) ;
#11845=CARTESIAN_POINT ( 'NONE',  ( -7.295229519525479489, 13.15279342069419499, -23.91310413417861369 ) ) ;
#11864=ADVANCED_FACE ( 'NONE', ( #11597 ), #7606, .F. ) ;
#11869=B_SPLINE_CURVE_WITH_KNOTS ( 'NONE', 3,
 ( #10057, #1367, #5234, #9105, #8151, #7187, #11065, #6427, #5670, #9597, #2746, #7441, #7632, #6604, #9539, #8458, #839, #12511, #4586, #9417 ),
 .UNSPECIFIED., .F., .F.,
 ( 4, 2, 2, 2, 2, 2, 2, 2, 2, 4 ),
 ( 0.007833776039060080451, 0.008812518928429134007, 0.009791261817798185829, 0.01028063326248271347, 0.01077000470716724112, 0.01174874759653627559, 0.01272749048590531007, 0.01370623337527434801, 0.01468497626464338249, 0.01566371915401241696 ),
 .UNSPECIFIED. ) ;
#11878=( LENGTH_UNIT ( ) NAMED_UNIT ( * ) SI_UNIT ( .MILLI., .METRE. ) );
#11883=CARTESIAN_POINT ( 'NONE',  ( -4.967291850848478241, 49.34246509418954929, -27.55594678612530757 ) ) ;
#11891=EDGE_LOOP ( 'NONE', ( #6616, #1968, #2422, #11456, #6625, #5479 ) ) ;
#11895=CARTESIAN_POINT ( 'NONE',  ( 7.531311395007206144, 13.38942809998023442, 26.97227661265244336 ) ) ;
#11902=CARTESIAN_POINT ( 'NONE',  ( 5.021458388981292487, 28.65403010179421983, 24.49227020900855933 ) ) ;
#11909=AXIS2_PLACEMENT_3D ( 'NONE', #10365, #2759, #6621 ) ;
#11915=CARTESIAN_POINT ( 'NONE',  ( 2.213389590484158731, 45.51360200414269741, -24.90224851187377553 ) ) ;
#11921=ORIENTED_EDGE ( 'NONE', *, *, #10383, .T. ) ;
#11924=ADVANCED_FACE ( 'NONE', ( #3667 ), #6770, .T. ) ;
#11937=ORIENTED_EDGE ( 'NONE', *, *, #5045, .T. ) ;
#11939=ORIENTED_EDGE ( 'NONE', *, *, #5368, .T. ) ;
#11951=CARTESIAN_POINT ( 'NONE',  ( -8.967015720386880773, 15.56160195868188545, 23.33709189419391805 ) ) ;
#11953=CARTESIAN_POINT ( 'NONE',  ( -9.467453437281745821, 23.23658378093145771, -26.35104892248523356 ) ) ;
#11954=ORIENTED_EDGE ( 'NONE', *, *, #5634, .F. ) ;
#11965=( NAMED_UNIT ( * ) PLANE_ANGLE_UNIT ( ) SI_UNIT ( $, .RADIAN. ) );
#11976=CARTESIAN_POINT ( 'NONE',  ( 3.764018802651051487, 53.30721710162806204, 24.71610890024348350 ) ) ;
#11982=CARTESIAN_POINT ( 'NONE',  ( -5.000000000000000000, 50.00000000000000000, 27.54995462791182348 ) ) ;
#11983=CARTESIAN_POINT ( 'NONE',  ( -2.217037138455994150, 45.50647851044359982, -24.90334479454202921 ) ) ;
#11986=CARTESIAN_POINT ( 'NONE',  ( -0.3301821175306443035, 55.00000000000001421, 25.00000000000000000 ) ) ;
#11995=ORIENTED_EDGE ( 'NONE', *, *, #10099, .T. ) ;
#12011=CARTESIAN_POINT ( 'NONE',  ( -9.983814731900727324, 19.34254964819328038, 22.91996290304706108 ) ) ;
#12013=CARTESIAN_POINT ( 'NONE',  ( -10.00000000000000355, 20.65909654603918355, -26.15339366124404563 ) ) ;
#12028=CARTESIAN_POINT ( 'NONE',  ( 4.999999999999999112, 50.32998418051842293, -24.49489742783177348 ) ) ;
#12043=CARTESIAN_POINT ( 'NONE',  ( -7.944152373534001832, 13.89170734695355058, 26.85206817267833657 ) ) ;
#12047=CARTESIAN_POINT ( 'NONE',  ( -5.000000000000000000, 50.00000000000000000, -24.49489742783178059 ) ) ;
#12053=CARTESIAN_POINT ( 'NONE',  ( 3.429011037612589670E-15, -4.262400816306111331E-15, 28.00000000000000355 ) ) ;
#12060=EDGE_LOOP ( 'NONE', ( #11320, #6900, #1156, #11638, #3779, #9974 ) ) ;
#12062=ORIENTED_EDGE ( 'NONE', *, *, #7656, .T. ) ;
#12068=CARTESIAN_POINT ( 'NONE',  ( -4.967628512179818046, 50.65508169058694676, -27.55588583811023895 ) ) ;
#12075=CARTESIAN_POINT ( 'NONE',  ( -7.536850167683876833, 13.39586159374066021, 23.84162237519015548 ) ) ;
#12088=CARTESIAN_POINT ( 'NONE',  ( -1.612909136089518691, 45.25592802960594696, 24.94976847917136453 ) ) ;
#12101=CARTESIAN_POINT ( 'NONE',  ( 10.00000000000000355, 20.00000000000000355, -28.00000000000000711 ) ) ;
#12110=ADVANCED_FACE ( 'NONE', ( #8173 ), #1386, .T. ) ;
#12117=CARTESIAN_POINT ( 'NONE',  ( 8.653999659896598473, 14.97853430653165319, -23.45497003317995421 ) ) ;
#12140=ORIENTED_EDGE ( 'NONE', *, *, #8777, .T. ) ;
#12148=CARTESIAN_POINT ( 'NONE',  ( 3.235823500505065287, 29.46772395162260594, 27.81419857650566385 ) ) ;
#12161=B_SPLINE_CURVE_WITH_KNOTS ( 'NONE', 3,
 ( #732, #12343, #3643, #11388, #8973, #6812, #32, #8025, #9803, #5046, #4083, #8778, #2117, #4917, #4150, #3071, #97, #1986 ),
 .UNSPECIFIED., .F., .F.,
 ( 4, 2, 2, 2, 2, 2, 2, 2, 4 ),
 ( 5.188175463412582976E-20, 0.0009797360301013575360, 0.001959472060202715072, 0.002939208090304072825, 0.003918944120405430144, 0.004898680150506787463, 0.005878416180608145650, 0.006858152210709502969, 0.007837888240810860288 ),
 .UNSPECIFIED. ) ;
#12179=APPLICATION_CONTEXT ( 'automotive_design' ) ;
#12185=LINE ( 'NONE', #3605, #8929 ) ;
#12187=DIRECTION ( 'NONE',  ( 0.000000000000000000, 0.000000000000000000, -1.000000000000000000 ) ) ;
#12190=CARTESIAN_POINT ( 'NONE',  ( -3.055901411439527759, 53.97113769530668037, -27.83409950995805460 ) ) ;
#12200=CARTESIAN_POINT ( 'NONE',  ( -5.841425570445385240, 28.12298897545994336, 27.38527483001175611 ) ) ;
#12202=EDGE_CURVE ( 'NONE', #6557, #8599, #2651, .T. ) ;
#12211=VERTEX_POINT ( 'NONE', #11394 ) ;
#12230=VERTEX_POINT ( 'NONE', #1933 ) ;
#12236=VECTOR ( 'NONE', #2683, 1000.000000000000000 ) ;
#12239=CARTESIAN_POINT ( 'NONE',  ( 8.963427797786382101, 15.55435157282535741, -23.33847234685102379 ) ) ;
#12245=CARTESIAN_POINT ( 'NONE',  ( 10.00000000000000355, 20.00000000000000355, 22.91287847477919826 ) ) ;
#12253=B_SPLINE_CURVE_WITH_KNOTS ( 'NONE', 3,
 ( #7019, #7139, #6256, #6075, #5247, #10957, #7079, #5313, #5062, #368, #10892, #10820, #11845, #3279, #3217, #7912, #8925, #4289, #1194, #6951, #8166, #2133, #11015, #6194, #4231, #242 ),
 .UNSPECIFIED., .F., .F.,
 ( 4, 2, 2, 2, 2, 2, 2, 2, 2, 2, 2, 2, 4 ),
 ( 0.01580552869034228605, 0.01679261472842853362, 0.01777970076651477771, 0.01975387284268728671, 0.02172804491885978878, 0.02271513095694604328, 0.02370221699503229779, 0.02567638907120481373, 0.02666347510929107170, 0.02765056114737732967, 0.02962473322354984562, 0.03061181926163610706, 0.03159890529972236156 ),
 .UNSPECIFIED. ) ;
#12256=ORIENTED_EDGE ( 'NONE', *, *, #11210, .T. ) ;
#12266=EDGE_CURVE ( 'NONE', #10006, #9751, #303, .T. ) ;
#12275=CARTESIAN_POINT ( 'NONE',  ( -2.505953076466797658, 45.67021871533034982, 24.87450930309000441 ) ) ;
#12285=CARTESIAN_POINT ( 'NONE',  ( 3.061616997868383043E-15, 0.000000000000000000, 25.00000000000000000 ) ) ;
#12302=CARTESIAN_POINT ( 'NONE',  ( 5.000000000000000000, 49.66865400565588828, 24.49489742783178414 ) ) ;
#12306=CARTESIAN_POINT ( 'NONE',  ( 5.340684424226280325E-17, 55.00000000000000000, -25.00000000000000000 ) ) ;
#12311=ADVANCED_BREP_SHAPE_REPRESENTATION ( '', ( #2064, #9021 ), #5775 ) ;
#12315=CARTESIAN_POINT ( 'NONE',  ( 9.657343816332662811, 22.61594140643868300, 23.05962942824199757 ) ) ;
#12321=DIRECTION ( 'NONE',  ( 0.000000000000000000, 0.000000000000000000, -1.000000000000000000 ) ) ;
#12323=CARTESIAN_POINT ( 'NONE',  ( 7.532348232781783892, 26.60942912475959332, -23.84307605514715434 ) ) ;
#12334=CARTESIAN_POINT ( 'NONE',  ( -4.744071016079746350, 48.38731143956220393, 24.54607980264442091 ) ) ;
#12339=ORIENTED_EDGE ( 'NONE', *, *, #8600, .T. ) ;
#12341=ORIENTED_EDGE ( 'NONE', *, *, #8808, .F. ) ;
#12343=CARTESIAN_POINT ( 'NONE',  ( -0.3313438815916917579, 54.99999999999998579, -25.00000000000000000 ) ) ;
#12357=EDGE_CURVE ( 'NONE', #1279, #6113, #9882, .T. ) ;
#12360=CARTESIAN_POINT ( 'NONE',  ( 0.000000000000000000, 0.000000000000000000, -28.00000000000000355 ) ) ;
#12364=CARTESIAN_POINT ( 'NONE',  ( 3.764226701178052803, 46.69296989397847852, 24.71608072572789538 ) ) ;
#12366=CARTESIAN_POINT ( 'NONE',  ( 3.061565168526138680E-15, 55.00000000000000000, 25.00000000000000000 ) ) ;
#12399=ORIENTED_EDGE ( 'NONE', *, *, #5893, .T. ) ;
#12410=CARTESIAN_POINT ( 'NONE',  ( 0.3311574161024399277, 54.99999999999999289, -28.00000000000000000 ) ) ;
#12425=CARTESIAN_POINT ( 'NONE',  ( 0.000000000000000000, 20.00000000000000355, -28.00000000000000711 ) ) ;
#12426=CARTESIAN_POINT ( 'NONE',  ( 10.00000000000000355, 20.00000000000000355, -22.91287847477919826 ) ) ;
#12427=EDGE_CURVE ( 'NONE', #1672, #10006, #7018, .T. ) ;
#12430=EDGE_LOOP ( 'NONE', ( #9082, #8330, #11921, #6977, #11556, #12256 ) ) ;
#12483=CARTESIAN_POINT ( 'NONE',  ( 0.3267965066156393039, 44.99999999999999289, -25.00000000000000355 ) ) ;
#12501=ORIENTED_EDGE ( 'NONE', *, *, #873, .T. ) ;
#12508=EDGE_CURVE ( 'NONE', #6404, #3714, #8991, .T. ) ;
#12509=CARTESIAN_POINT ( 'NONE',  ( 9.935507569286025742, 21.31398369048515562, -22.94135581966985526 ) ) ;
#12511=CARTESIAN_POINT ( 'NONE',  ( 0.6583504323226527788, 45.03273075554383098, -27.99410254389716357 ) ) ;
#12525=CARTESIAN_POINT ( 'NONE',  ( -3.242423582264189807, 29.46551675503955536, -24.79088612835948879 ) ) ;
#12585=COLOUR_RGB('Black',0.12,0.14,0.17);
#12586=FILL_AREA_STYLE_COLOUR('',#12585);
#12587=FILL_AREA_STYLE('',(#12586));
#12588=SURFACE_STYLE_FILL_AREA(#12587);
#12589=SURFACE_SIDE_STYLE('',(#12588));
#12590=SURFACE_STYLE_USAGE(.BOTH.,#12589);
#12591=PRESENTATION_STYLE_ASSIGNMENT((#12590));
ENDSEC;
END-ISO-10303-21;
